ISO-10303-21;
HEADER;
FILE_DESCRIPTION (('STEP AP214'),
    '1' );
FILE_NAME ('Grease Lubrication Injection Nipple.step',
    '2026-10-09T12:49:55',
    ( '' ),
    ( '' ),
    'SwSTEP 2.0',
    'SolidWorks 2026',
    '' );
FILE_SCHEMA (( 'AUTOMOTIVE_DESIGN' ));
ENDSEC;

DATA;
#4=CARTESIAN_POINT ( 'NONE',  ( 227.3999999999999773, -2.172755033604258923, 3.940702420120982374 ) ) ;
#7=CARTESIAN_POINT ( 'NONE',  ( 222.8706404512946904, 0.000000000000000000, 0.000000000000000000 ) ) ;
#8=EDGE_LOOP ( 'NONE', ( #2627, #6093, #4363, #303 ) ) ;
#10=CONICAL_SURFACE ( 'NONE', #3613, 1.750000000000000000, 0.4188790204786330129 ) ;
#14=EDGE_CURVE ( 'NONE', #2438, #5570, #3411, .T. ) ;
#34=AXIS2_PLACEMENT_3D ( 'NONE', #11717, #7639, #3504 ) ;
#56=CARTESIAN_POINT ( 'NONE',  ( 220.3999999999999773, 2.249562960690858038, -0.04434507737934524629 ) ) ;
#106=FACE_OUTER_BOUND ( 'NONE', #3222, .T. ) ;
#109=CARTESIAN_POINT ( 'NONE',  ( 234.3487510399341716, 2.474519256759935448, -0.04877958511727960994 ) ) ;
#163=AXIS2_PLACEMENT_3D ( 'NONE', #4831, #2895, #11790 ) ;
#170=CARTESIAN_POINT ( 'NONE',  ( 226.1499999999999773, 0.000000000000000000, 0.000000000000000000 ) ) ;
#172=ORIENTED_EDGE ( 'NONE', *, *, #9218, .F. ) ;
#175=FACE_OUTER_BOUND ( 'NONE', #11352, .T. ) ;
#183=ORIENTED_EDGE ( 'NONE', *, *, #8273, .T. ) ;
#204=VERTEX_POINT ( 'NONE', #489 ) ;
#219=PRODUCT ( 'Grease Lubrication Injection Nipple', 'Grease Lubrication Injection Nipple', '', ( #6400 ) ) ;
#231=DIRECTION ( 'NONE',  ( 1.000000000000000000, 0.000000000000000000, 0.000000000000000000 ) ) ;
#236=CARTESIAN_POINT ( 'NONE',  ( 222.0845275804282153, 0.000000000000000000, 0.000000000000000000 ) ) ;
#246=DIRECTION ( 'NONE',  ( 0.9135454576426030870, 0.4066576386751317163, -0.008016341293427224970 ) ) ;
#278=EDGE_CURVE ( 'NONE', #2702, #9134, #8362, .T. ) ;
#298=CARTESIAN_POINT ( 'NONE',  ( 227.3999999999999773, -0.1024105694488001289, -5.195143123655522110 ) ) ;
#303=ORIENTED_EDGE ( 'NONE', *, *, #10671, .T. ) ;
#308=CARTESIAN_POINT ( 'NONE',  ( 224.4939760857161843, 0.000000000000000000, 0.000000000000000000 ) ) ;
#314=FACE_OUTER_BOUND ( 'NONE', #7559, .T. ) ;
#328=FACE_OUTER_BOUND ( 'NONE', #9057, .T. ) ;
#344=DIRECTION ( 'NONE',  ( 0.9135454576426033091, -0.4066576386751313277, 0.008016341293427268339 ) ) ;
#347=LINE ( 'NONE', #4396, #11357 ) ;
#364=EDGE_LOOP ( 'NONE', ( #8503, #2474 ) ) ;
#379=VERTEX_POINT ( 'NONE', #7675 ) ;
#394=CARTESIAN_POINT ( 'NONE',  ( 227.3999999999999773, -0.1024105694488001289, -5.195143123655522110 ) ) ;
#411=AXIS2_PLACEMENT_3D ( 'NONE', #8959, #7961, #12028 ) ;
#429=DIRECTION ( 'NONE',  ( 1.000000000000000000, 0.000000000000000000, 0.000000000000000000 ) ) ;
#431=VERTEX_POINT ( 'NONE', #8744 ) ;
#440=DIRECTION ( 'NONE',  ( 0.000000000000000000, 0.9998057603070480415, -0.01970892327970899874 ) ) ;
#467=ORIENTED_EDGE ( 'NONE', *, *, #10070, .F. ) ;
#474=DIRECTION ( 'NONE',  ( 0.000000000000000000, 0.9998057603070481525, -0.01970892327970900221 ) ) ;
#489=CARTESIAN_POINT ( 'NONE',  ( 235.0999999999999943, -1.949621232598743648, 0.03843240039543278225 ) ) ;
#490=AXIS2_PLACEMENT_3D ( 'NONE', #7345, #7278, #6481 ) ;
#521=EDGE_CURVE ( 'NONE', #5366, #4133, #12274, .T. ) ;
#530=VECTOR ( 'NONE', #9464, 1000.000000000000227 ) ;
#541=CIRCLE ( 'NONE', #9685, 0.7999999999999999334 ) ;
#543=EDGE_CURVE ( 'NONE', #8768, #1281, #5197, .T. ) ;
#582=CARTESIAN_POINT ( 'NONE',  ( 227.3999999999999773, -4.550331206106116078, -2.508881407069070590 ) ) ;
#586=DIRECTION ( 'NONE',  ( 1.000000000000000000, 0.000000000000000000, 0.000000000000000000 ) ) ;
#615=CIRCLE ( 'NONE', #3368, 3.000000000000000000 ) ;
#628=ORIENTED_EDGE ( 'NONE', *, *, #6008, .T. ) ;
#645=CIRCLE ( 'NONE', #5753, 1.750000000000000000 ) ;
#655=EDGE_CURVE ( 'NONE', #11681, #11485, #6209, .T. ) ;
#657=EDGE_CURVE ( 'NONE', #926, #2842, #5947, .T. ) ;
#665=FACE_BOUND ( 'NONE', #7591, .T. ) ;
#680=DIRECTION ( 'NONE',  ( 0.000000000000000000, 0.9998057603070481525, -0.01970892327970899874 ) ) ;
#683=EDGE_CURVE ( 'NONE', #1246, #5570, #3794, .T. ) ;
#701=DIRECTION ( 'NONE',  ( 0.000000000000000000, 0.000000000000000000, -1.000000000000000000 ) ) ;
#729=ORIENTED_EDGE ( 'NONE', *, *, #2530, .F. ) ;
#751=CIRCLE ( 'NONE', #9895, 4.500000000000000000 ) ;
#769=CARTESIAN_POINT ( 'NONE',  ( 235.4000000000000057, 0.000000000000000000, 0.000000000000000000 ) ) ;
#775=EDGE_CURVE ( 'NONE', #4133, #3138, #10532, .T. ) ;
#776=ORIENTED_EDGE ( 'NONE', *, *, #6811, .T. ) ;
#788=LINE ( 'NONE', #6925, #4779 ) ;
#798=FACE_OUTER_BOUND ( 'NONE', #12920, .T. ) ;
#805=AXIS2_PLACEMENT_3D ( 'NONE', #6711, #10765, #10635 ) ;
#807=ORIENTED_EDGE ( 'NONE', *, *, #8174, .F. ) ;
#809=CARTESIAN_POINT ( 'NONE',  ( 226.7234983661818717, 3.822755691033211001, -0.07535703595917098152 ) ) ;
#824=AXIS2_PLACEMENT_3D ( 'NONE', #9221, #9423, #2082 ) ;
#838=ORIENTED_EDGE ( 'NONE', *, *, #13038, .T. ) ;
#842=CONICAL_SURFACE ( 'NONE', #2113, 3.823498366181860231, 0.7853981633974476129 ) ;
#853=ORIENTED_EDGE ( 'NONE', *, *, #7856, .T. ) ;
#863=PLANE ( 'NONE',  #11658 ) ;
#876=DIRECTION ( 'NONE',  ( 0.000000000000000000, 0.9998057603070481525, -0.01970892327970900221 ) ) ;
#887=DIRECTION ( 'NONE',  ( 1.000000000000000000, 0.000000000000000000, 0.000000000000000000 ) ) ;
#903=ORIENTED_EDGE ( 'NONE', *, *, #3096, .F. ) ;
#926=VERTEX_POINT ( 'NONE', #12719 ) ;
#932=AXIS2_PLACEMENT_3D ( 'NONE', #1531, #10591, #3525 ) ;
#938=EDGE_CURVE ( 'NONE', #8755, #4344, #11803, .T. ) ;
#954=FACE_OUTER_BOUND ( 'NONE', #7686, .T. ) ;
#964=CONICAL_SURFACE ( 'NONE', #10965, 3.000000000000000000, 0.7853981633974461696 ) ;
#968=DIRECTION ( 'NONE',  ( -0.000000000000000000, 0.01970892327970912364, 0.9998057603070482635 ) ) ;
#978=DIRECTION ( 'NONE',  ( 0.000000000000000000, 0.9998057603070481525, -0.01970892327970899874 ) ) ;
#983=PLANE ( 'NONE',  #9235 ) ;
#987=ADVANCED_FACE ( 'NONE', ( #665, #10924 ), #6799, .F. ) ;
#1000=DIRECTION ( 'NONE',  ( 0.000000000000000000, -0.9998057603070481525, 0.01970892327970883220 ) ) ;
#1013=CIRCLE ( 'NONE', #2494, 2.475000000000000089 ) ;
#1039=CARTESIAN_POINT ( 'NONE',  ( 235.4000000000000057, -2.999417280921144346, 0.05912676983912699968 ) ) ;
#1053=ORIENTED_EDGE ( 'NONE', *, *, #543, .T. ) ;
#1065=FACE_OUTER_BOUND ( 'NONE', #4750, .T. ) ;
#1070=CARTESIAN_POINT ( 'NONE',  ( 222.8706404512946904, 3.349349297028606731, -0.06602489298702507448 ) ) ;
#1074=EDGE_CURVE ( 'NONE', #5758, #1246, #3524, .T. ) ;
#1087=CARTESIAN_POINT ( 'NONE',  ( 226.7234983661818717, 0.000000000000000000, 0.000000000000000000 ) ) ;
#1098=ORIENTED_EDGE ( 'NONE', *, *, #3769, .F. ) ;
#1122=ORIENTED_EDGE ( 'NONE', *, *, #12541, .F. ) ;
#1132=AXIS2_PLACEMENT_3D ( 'NONE', #7511, #5571, #9628 ) ;
#1139=DIRECTION ( 'NONE',  ( 0.000000000000000000, -0.8757116489157734662, -0.4828344519120573719 ) ) ;
#1150=ORIENTED_EDGE ( 'NONE', *, *, #12559, .F. ) ;
#1153=EDGE_LOOP ( 'NONE', ( #5138, #8243, #2584, #1302 ) ) ;
#1211=DIRECTION ( 'NONE',  ( 0.000000000000000000, 0.8757116489157734662, 0.4828344519120573719 ) ) ;
#1223=TOROIDAL_SURFACE ( 'NONE', #12290, 2.200000000000000178, 0.8000000000000000444 ) ;
#1237=LINE ( 'NONE', #8445, #7442 ) ;
#1246=VERTEX_POINT ( 'NONE', #11720 ) ;
#1281=VERTEX_POINT ( 'NONE', #6524 ) ;
#1289=FACE_OUTER_BOUND ( 'NONE', #12054, .T. ) ;
#1302=ORIENTED_EDGE ( 'NONE', *, *, #2252, .F. ) ;
#1306=CARTESIAN_POINT ( 'NONE',  ( 226.7234983661818717, 0.000000000000000000, 0.000000000000000000 ) ) ;
#1311=AXIS2_PLACEMENT_3D ( 'NONE', #11230, #5029, #2097 ) ;
#1313=FACE_OUTER_BOUND ( 'NONE', #12183, .T. ) ;
#1315=ORIENTED_EDGE ( 'NONE', *, *, #3096, .T. ) ;
#1317=CARTESIAN_POINT ( 'NONE',  ( 227.3999999999999773, -2.326370887777457153, -3.852012265362291465 ) ) ;
#1322=CARTESIAN_POINT ( 'NONE',  ( 235.4000000000000057, 0.000000000000000000, 0.000000000000000000 ) ) ;
#1337=CIRCLE ( 'NONE', #4945, 4.000000000000000000 ) ;
#1338=CARTESIAN_POINT ( 'NONE',  ( 227.3999999999999773, -4.447920636657316074, 2.686261716586446635 ) ) ;
#1353=EDGE_CURVE ( 'NONE', #3016, #3738, #10239, .T. ) ;
#1371=VECTOR ( 'NONE', #3321, 1000.000000000000114 ) ;
#1373=CARTESIAN_POINT ( 'NONE',  ( 235.4000000000000057, 0.000000000000000000, 0.000000000000000000 ) ) ;
#1387=DIRECTION ( 'NONE',  ( 1.000000000000000000, 0.000000000000000000, 0.000000000000000000 ) ) ;
#1400=CARTESIAN_POINT ( 'NONE',  ( 235.4000000000000057, 3.999223041228192610, -0.07883569311883599495 ) ) ;
#1436=DIRECTION ( 'NONE',  ( 1.000000000000000000, 0.000000000000000000, 0.000000000000000000 ) ) ;
#1441=ORIENTED_EDGE ( 'NONE', *, *, #2466, .F. ) ;
#1446=FACE_OUTER_BOUND ( 'NONE', #2903, .T. ) ;
#1470=DIRECTION ( 'NONE',  ( 1.000000000000000000, 0.000000000000000000, 0.000000000000000000 ) ) ;
#1515=FACE_OUTER_BOUND ( 'NONE', #11834, .T. ) ;
#1531=CARTESIAN_POINT ( 'NONE',  ( 235.4000000000000057, 0.1024105694487990881, 5.195143123655512341 ) ) ;
#1546=LINE ( 'NONE', #7609, #12096 ) ;
#1554=CARTESIAN_POINT ( 'NONE',  ( 222.0845275804282153, 1.749660080537334128, -0.03449061573949074866 ) ) ;
#1564=AXIS2_PLACEMENT_3D ( 'NONE', #769, #9821, #9893 ) ;
#1590=DIRECTION ( 'NONE',  ( -0.000000000000000000, 0.01970892327970912364, 0.9998057603070482635 ) ) ;
#1597=ORIENTED_EDGE ( 'NONE', *, *, #7049, .T. ) ;
#1603=EDGE_CURVE ( 'NONE', #11485, #10920, #1237, .T. ) ;
#1611=TOROIDAL_SURFACE ( 'NONE', #3085, 6.053020646647509828, 3.153020646647509917 ) ;
#1622=ORIENTED_EDGE ( 'NONE', *, *, #655, .T. ) ;
#1634=FACE_OUTER_BOUND ( 'NONE', #2304, .T. ) ;
#1653=ORIENTED_EDGE ( 'NONE', *, *, #8666, .T. ) ;
#1654=ADVANCED_FACE ( 'NONE', ( #954 ), #8954, .F. ) ;
#1660=DIRECTION ( 'NONE',  ( 0.000000000000000000, -0.01970892327970899874, -0.9998057603070481525 ) ) ;
#1663=DIRECTION ( 'NONE',  ( 0.000000000000000000, 0.9998057603070481525, -0.01970892327970899874 ) ) ;
#1691=VERTEX_POINT ( 'NONE', #5891 ) ;
#1695=AXIS2_PLACEMENT_3D ( 'NONE', #8157, #5070, #4881 ) ;
#1702=VECTOR ( 'NONE', #8523, 1000.000000000000000 ) ;
#1705=ORIENTED_EDGE ( 'NONE', *, *, #3097, .F. ) ;
#1731=FACE_OUTER_BOUND ( 'NONE', #10353, .T. ) ;
#1735=EDGE_CURVE ( 'NONE', #7894, #5758, #7229, .T. ) ;
#1743=CARTESIAN_POINT ( 'NONE',  ( 235.4000000000000057, -4.447920636657316074, 2.686261716586446635 ) ) ;
#1756=ORIENTED_EDGE ( 'NONE', *, *, #2125, .T. ) ;
#1800=LINE ( 'NONE', #7724, #9130 ) ;
#1831=EDGE_LOOP ( 'NONE', ( #11112, #1756, #1653 ) ) ;
#1873=ORIENTED_EDGE ( 'NONE', *, *, #12559, .T. ) ;
#1876=DIRECTION ( 'NONE',  ( 0.000000000000000000, -0.8757116489157734662, -0.4828344519120573719 ) ) ;
#1893=VECTOR ( 'NONE', #4417, 1000.000000000000227 ) ;
#1898=( NAMED_UNIT ( * ) SI_UNIT ( $, .STERADIAN. ) SOLID_ANGLE_UNIT ( ) );
#1959=AXIS2_PLACEMENT_3D ( 'NONE', #4036, #2171, #8184 ) ;
#1974=CARTESIAN_POINT ( 'NONE',  ( 226.1499999999999773, -1.749660080537334572, 0.03449061573949096376 ) ) ;
#1983=DIRECTION ( 'NONE',  ( -0.000000000000000000, 0.8560027256360644987, -0.5169713083949903920 ) ) ;
#2008=DIRECTION ( 'NONE',  ( 0.000000000000000000, -0.9998057603070481525, 0.01970892327970899874 ) ) ;
#2030=ORIENTED_EDGE ( 'NONE', *, *, #8271, .T. ) ;
#2044=ORIENTED_EDGE ( 'NONE', *, *, #657, .T. ) ;
#2054=DIRECTION ( 'NONE',  ( 0.000000000000000000, 0.9998057603070481525, -0.01970892327970899874 ) ) ;
#2064=ORIENTED_EDGE ( 'NONE', *, *, #5815, .F. ) ;
#2082=DIRECTION ( 'NONE',  ( 0.000000000000000000, 0.9998057603070480415, -0.01970892327970899874 ) ) ;
#2092=VECTOR ( 'NONE', #5127, 1000.000000000000227 ) ;
#2097=DIRECTION ( 'NONE',  ( 0.000000000000000000, 0.9998057603070481525, -0.01970892327970900221 ) ) ;
#2113=AXIS2_PLACEMENT_3D ( 'NONE', #1306, #6378, #9442 ) ;
#2118=CARTESIAN_POINT ( 'NONE',  ( 235.4000000000000057, -0.1024105694488001289, -5.195143123655522110 ) ) ;
#2125=EDGE_CURVE ( 'NONE', #3954, #3345, #11078, .T. ) ;
#2130=ORIENTED_EDGE ( 'NONE', *, *, #8273, .F. ) ;
#2148=CARTESIAN_POINT ( 'NONE',  ( 222.0845275804282153, 1.749660080537334128, -0.03449061573949074866 ) ) ;
#2159=ORIENTED_EDGE ( 'NONE', *, *, #6882, .F. ) ;
#2167=CARTESIAN_POINT ( 'NONE',  ( 229.9000000000000057, 4.550331206106116078, 2.508881407069060376 ) ) ;
#2171=DIRECTION ( 'NONE',  ( 1.000000000000000000, 0.000000000000000000, 0.000000000000000000 ) ) ;
#2173=LINE ( 'NONE', #7116, #7927 ) ;
#2174=AXIS2_PLACEMENT_3D ( 'NONE', #12269, #4260, #3186 ) ;
#2176=ORIENTED_EDGE ( 'NONE', *, *, #9731, .T. ) ;
#2190=COLOUR_RGB ( '', 0.31764706, 0.68627451, 0.89019608) ;
#2195=CIRCLE ( 'NONE', #9866, 1.750000000000000000 ) ;
#2218=CIRCLE ( 'NONE', #8197, 3.153020646647511249 ) ;
#2228=EDGE_CURVE ( 'NONE', #8768, #2870, #12765, .T. ) ;
#2244=DIRECTION ( 'NONE',  ( 0.000000000000000000, 0.01970892327970899874, 0.9998057603070481525 ) ) ;
#2246=ADVANCED_FACE ( 'NONE', ( #1446 ), #3391, .F. ) ;
#2252=EDGE_CURVE ( 'NONE', #5570, #1246, #8724, .T. ) ;
#2260=ORIENTED_EDGE ( 'NONE', *, *, #14, .T. ) ;
#2283=DIRECTION ( 'NONE',  ( 0.000000000000000000, 0.9998057603070481525, -0.01970892327970900221 ) ) ;
#2290=EDGE_LOOP ( 'NONE', ( #10173, #6761, #12594, #2808 ) ) ;
#2304=EDGE_LOOP ( 'NONE', ( #6718, #6456, #12577, #729 ) ) ;
#2318=ADVANCED_FACE ( 'NONE', ( #328 ), #7387, .F. ) ;
#2324=ADVANCED_FACE ( 'NONE', ( #1515 ), #12456, .T. ) ;
#2334=CARTESIAN_POINT ( 'NONE',  ( 226.1499999999999773, 0.000000000000000000, 0.000000000000000000 ) ) ;
#2344=CIRCLE ( 'NONE', #8732, 3.153020646647511249 ) ;
#2350=FACE_OUTER_BOUND ( 'NONE', #4082, .T. ) ;
#2356=CARTESIAN_POINT ( 'NONE',  ( 235.4000000000000057, 0.000000000000000000, 0.000000000000000000 ) ) ;
#2362=CARTESIAN_POINT ( 'NONE',  ( 222.0845275804282153, 0.000000000000000000, 0.000000000000000000 ) ) ;
#2368=DIRECTION ( 'NONE',  ( 1.000000000000000000, 0.000000000000000000, 0.000000000000000000 ) ) ;
#2373=CIRCLE ( 'NONE', #6848, 3.350000000000000089 ) ;
#2390=AXIS2_PLACEMENT_3D ( 'NONE', #7, #11333, #11133 ) ;
#2391=ADVANCED_FACE ( 'NONE', ( #5645 ), #3369, .F. ) ;
#2409=ORIENTED_EDGE ( 'NONE', *, *, #2466, .T. ) ;
#2411=DIRECTION ( 'NONE',  ( 0.000000000000000000, 0.01970892327970883220, 0.9998057603070481525 ) ) ;
#2422=ORIENTED_EDGE ( 'NONE', *, *, #5347, .F. ) ;
#2428=EDGE_LOOP ( 'NONE', ( #5143, #2422, #4815, #3360, #6172, #5954 ) ) ;
#2433=AXIS2_PLACEMENT_3D ( 'NONE', #11709, #10824, #2682 ) ;
#2438=VERTEX_POINT ( 'NONE', #11526 ) ;
#2444=CIRCLE ( 'NONE', #12655, 0.7999999999999999334 ) ;
#2453=AXIS2_PLACEMENT_3D ( 'NONE', #8178, #3090, #6372 ) ;
#2457=DIRECTION ( 'NONE',  ( -1.000000000000000000, 0.000000000000000000, 0.000000000000000000 ) ) ;
#2466=EDGE_CURVE ( 'NONE', #11681, #431, #10518, .T. ) ;
#2468=CARTESIAN_POINT ( 'NONE',  ( 226.7234983661818717, -3.822755691033211001, 0.07535703595917145337 ) ) ;
#2474=ORIENTED_EDGE ( 'NONE', *, *, #938, .F. ) ;
#2475=CARTESIAN_POINT ( 'NONE',  ( 235.0999999999999943, -2.749465840844381948, 0.05419953901920007699 ) ) ;
#2494=AXIS2_PLACEMENT_3D ( 'NONE', #3572, #10714, #11722 ) ;
#2495=CARTESIAN_POINT ( 'NONE',  ( 235.4000000000000057, 4.550331206106116078, 2.508881407069060376 ) ) ;
#2513=DIRECTION ( 'NONE',  ( 0.000000000000000000, -0.8757116489157734662, -0.4828344519120573719 ) ) ;
#2525=DIRECTION ( 'NONE',  ( -1.000000000000000000, 0.000000000000000000, 0.000000000000000000 ) ) ;
#2530=EDGE_CURVE ( 'NONE', #6733, #4344, #9836, .T. ) ;
#2541=AXIS2_PLACEMENT_3D ( 'NONE', #1373, #4367, #440 ) ;
#2557=CARTESIAN_POINT ( 'NONE',  ( 224.4939760857161843, 0.000000000000000000, 0.000000000000000000 ) ) ;
#2561=CARTESIAN_POINT ( 'NONE',  ( 220.3999999999999773, -2.249562960690858038, 0.04434507737934551691 ) ) ;
#2571=DIRECTION ( 'NONE',  ( 0.000000000000000000, 0.9998057603070481525, -0.01970892327970899874 ) ) ;
#2581=ORIENTED_EDGE ( 'NONE', *, *, #5256, .F. ) ;
#2583=CARTESIAN_POINT ( 'NONE',  ( 235.4000000000000057, -4.550331206106116078, -2.508881407069070590 ) ) ;
#2584=ORIENTED_EDGE ( 'NONE', *, *, #9641, .T. ) ;
#2587=CARTESIAN_POINT ( 'NONE',  ( 220.3999999999999773, -0.01970892327970899874, -0.9998057603070481525 ) ) ;
#2590=CARTESIAN_POINT ( 'NONE',  ( 235.4000000000000057, -2.999417280921144346, 0.05912676983912736745 ) ) ;
#2609=DIRECTION ( 'NONE',  ( 0.9135454576426033091, 0.4066576386751313277, -0.008016341293427218032 ) ) ;
#2624=EDGE_CURVE ( 'NONE', #379, #12401, #2373, .T. ) ;
#2627=ORIENTED_EDGE ( 'NONE', *, *, #12425, .F. ) ;
#2628=FACE_OUTER_BOUND ( 'NONE', #3601, .T. ) ;
#2633=CARTESIAN_POINT ( 'NONE',  ( 235.4000000000000057, 2.749465840844381948, -0.05419953901919974393 ) ) ;
#2651=DIRECTION ( 'NONE',  ( 1.000000000000000000, 0.000000000000000000, 0.000000000000000000 ) ) ;
#2659=AXIS2_PLACEMENT_3D ( 'NONE', #10495, #429, #5428 ) ;
#2678=LINE ( 'NONE', #8759, #11140 ) ;
#2682=DIRECTION ( 'NONE',  ( 0.000000000000000000, -0.9998057603070481525, 0.01970892327970899874 ) ) ;
#2695=FACE_OUTER_BOUND ( 'NONE', #2428, .T. ) ;
#2702=VERTEX_POINT ( 'NONE', #1974 ) ;
#2705=EDGE_CURVE ( 'NONE', #9399, #3954, #8181, .T. ) ;
#2713=FACE_OUTER_BOUND ( 'NONE', #12815, .T. ) ;
#2724=EDGE_CURVE ( 'NONE', #9134, #3138, #7688, .T. ) ;
#2729=CARTESIAN_POINT ( 'NONE',  ( 224.4939760857161843, 0.000000000000000000, 0.000000000000000000 ) ) ;
#2732=CARTESIAN_POINT ( 'NONE',  ( 224.4939760857161843, 0.000000000000000000, 0.000000000000000000 ) ) ;
#2738=ORIENTED_EDGE ( 'NONE', *, *, #5494, .F. ) ;
#2768=CARTESIAN_POINT ( 'NONE',  ( 235.4000000000000057, 4.447920636657316074, -2.686261716586451520 ) ) ;
#2786=EDGE_CURVE ( 'NONE', #6733, #5475, #7059, .T. ) ;
#2807=ORIENTED_EDGE ( 'NONE', *, *, #8666, .F. ) ;
#2808=ORIENTED_EDGE ( 'NONE', *, *, #7306, .F. ) ;
#2828=CARTESIAN_POINT ( 'NONE',  ( 229.9000000000000057, 4.447920636657316074, -2.686261716586451520 ) ) ;
#2842=VERTEX_POINT ( 'NONE', #2167 ) ;
#2868=CIRCLE ( 'NONE', #12672, 2.250000000000000000 ) ;
#2870=VERTEX_POINT ( 'NONE', #6442 ) ;
#2874=ORIENTED_EDGE ( 'NONE', *, *, #2705, .T. ) ;
#2885=EDGE_CURVE ( 'NONE', #3138, #3016, #9619, .T. ) ;
#2891=DIRECTION ( 'NONE',  ( 1.000000000000000000, 0.000000000000000000, 0.000000000000000000 ) ) ;
#2895=DIRECTION ( 'NONE',  ( -1.000000000000000000, 0.000000000000000000, 0.000000000000000000 ) ) ;
#2903=EDGE_LOOP ( 'NONE', ( #7717, #10571, #7957, #9497 ) ) ;
#2920=ORIENTED_EDGE ( 'NONE', *, *, #2125, .F. ) ;
#2934=EDGE_CURVE ( 'NONE', #4597, #5366, #2195, .T. ) ;
#2964=CARTESIAN_POINT ( 'NONE',  ( 235.4000000000000057, 0.000000000000000000, 0.000000000000000000 ) ) ;
#2992=CARTESIAN_POINT ( 'NONE',  ( 235.0999999999999943, 0.000000000000000000, 0.000000000000000000 ) ) ;
#3016=VERTEX_POINT ( 'NONE', #12693 ) ;
#3058=FACE_OUTER_BOUND ( 'NONE', #8356, .T. ) ;
#3080=EDGE_CURVE ( 'NONE', #2842, #11681, #10821, .T. ) ;
#3085=AXIS2_PLACEMENT_3D ( 'NONE', #308, #6240, #3346 ) ;
#3089=EDGE_LOOP ( 'NONE', ( #8659, #4063, #2807, #2159, #7868 ) ) ;
#3090=DIRECTION ( 'NONE',  ( 0.000000000000000000, -0.01970892327970900221, -0.9998057603070482635 ) ) ;
#3096=EDGE_CURVE ( 'NONE', #3954, #5655, #2678, .T. ) ;
#3097=EDGE_CURVE ( 'NONE', #3301, #3428, #6470, .T. ) ;
#3123=CARTESIAN_POINT ( 'NONE',  ( 229.9000000000000057, 0.4213317357727130452, -4.906371323945101004 ) ) ;
#3135=ADVANCED_FACE ( 'NONE', ( #5836 ), #7691, .T. ) ;
#3138=VERTEX_POINT ( 'NONE', #11770 ) ;
#3149=CIRCLE ( 'NONE', #12735, 3.153020646647511249 ) ;
#3153=ORIENTED_EDGE ( 'NONE', *, *, #11196, .F. ) ;
#3154=DIRECTION ( 'NONE',  ( 0.9135454576426030870, -0.4066576386751317163, 0.008016341293427277012 ) ) ;
#3186=DIRECTION ( 'NONE',  ( 0.000000000000000000, 0.9998057603070481525, -0.01970892327970899874 ) ) ;
#3202=ORIENTED_EDGE ( 'NONE', *, *, #5128, .T. ) ;
#3213=ADVANCED_FACE ( 'NONE', ( #4816 ), #9446, .T. ) ;
#3221=LINE ( 'NONE', #4361, #6302 ) ;
#3222=EDGE_LOOP ( 'NONE', ( #9599, #7422, #10241, #8859 ) ) ;
#3231=AXIS2_PLACEMENT_3D ( 'NONE', #8212, #1000, #11402 ) ;
#3244=DIRECTION ( 'NONE',  ( -0.000000000000000000, -0.5169713083949905030, -0.8560027256360646097 ) ) ;
#3245=TOROIDAL_SURFACE ( 'NONE', #7303, 2.200000000000000178, 0.8000000000000000444 ) ;
#3275=DIRECTION ( 'NONE',  ( 0.7071067811865470176, -0.7069694329824861567, 0.01393631330096774257 ) ) ;
#3280=ORIENTED_EDGE ( 'NONE', *, *, #2624, .F. ) ;
#3283=DIRECTION ( 'NONE',  ( 1.000000000000000000, 0.000000000000000000, 0.000000000000000000 ) ) ;
#3301=VERTEX_POINT ( 'NONE', #5335 ) ;
#3304=CARTESIAN_POINT ( 'NONE',  ( 227.3999999999999773, 0.000000000000000000, 0.000000000000000000 ) ) ;
#3321=DIRECTION ( 'NONE',  ( 0.7071067811865470176, 0.7069694329824861567, -0.01393631330096765583 ) ) ;
#3336=LINE ( 'NONE', #7226, #12538 ) ;
#3345=VERTEX_POINT ( 'NONE', #1317 ) ;
#3346=DIRECTION ( 'NONE',  ( 0.000000000000000000, 0.9998057603070481525, -0.01970892327970900221 ) ) ;
#3351=FACE_OUTER_BOUND ( 'NONE', #12237, .T. ) ;
#3353=CARTESIAN_POINT ( 'NONE',  ( 235.4000000000000057, 4.550331206106116078, 2.508881407069060376 ) ) ;
#3360=ORIENTED_EDGE ( 'NONE', *, *, #655, .F. ) ;
#3368=AXIS2_PLACEMENT_3D ( 'NONE', #10058, #11058, #9261 ) ;
#3369=CYLINDRICAL_SURFACE ( 'NONE', #4037, 2.749999999999999556 ) ;
#3374=CIRCLE ( 'NONE', #411, 2.749999999999999556 ) ;
#3391=TOROIDAL_SURFACE ( 'NONE', #9184, 6.053020646647509828, 3.153020646647509917 ) ;
#3411=LINE ( 'NONE', #8233, #3468 ) ;
#3415=CARTESIAN_POINT ( 'NONE',  ( 227.3999999999999773, -4.499125921381716076, 0.08869015475868961829 ) ) ;
#3427=AXIS2_PLACEMENT_3D ( 'NONE', #10158, #5161, #10101 ) ;
#3428=VERTEX_POINT ( 'NONE', #7252 ) ;
#3434=DIRECTION ( 'NONE',  ( 1.000000000000000000, 0.000000000000000000, 0.000000000000000000 ) ) ;
#3437=DIRECTION ( 'NONE',  ( 0.000000000000000000, 0.9998057603070481525, -0.01970892327970899874 ) ) ;
#3452=EDGE_CURVE ( 'NONE', #3428, #12401, #3149, .T. ) ;
#3461=PLANE ( 'NONE',  #4525 ) ;
#3468=VECTOR ( 'NONE', #10214, 1000.000000000000114 ) ;
#3504=DIRECTION ( 'NONE',  ( 0.000000000000000000, -0.9998057603070481525, 0.01970892327970899874 ) ) ;
#3524=LINE ( 'NONE', #11805, #8707 ) ;
#3525=DIRECTION ( 'NONE',  ( 1.000000000000000000, 0.000000000000000000, 0.000000000000000000 ) ) ;
#3526=LINE ( 'NONE', #5664, #9571 ) ;
#3555=VECTOR ( 'NONE', #9862, 1000.000000000000000 ) ;
#3559=SHAPE_REPRESENTATION_RELATIONSHIP ( 'NONE' , 'NONE' ,  #12521, #6669 ) ;
#3572=CARTESIAN_POINT ( 'NONE',  ( 234.3487510399341716, 0.000000000000000000, 0.000000000000000000 ) ) ;
#3601=EDGE_LOOP ( 'NONE', ( #3153, #2260, #7322, #12971 ) ) ;
#3609=DIRECTION ( 'NONE',  ( 1.000000000000000000, 0.000000000000000000, 0.000000000000000000 ) ) ;
#3613=AXIS2_PLACEMENT_3D ( 'NONE', #9860, #9786, #6740 ) ;
#3622=LINE ( 'NONE', #8762, #7650 ) ;
#3626=( NAMED_UNIT ( * ) PLANE_ANGLE_UNIT ( ) SI_UNIT ( $, .RADIAN. ) );
#3634=VERTEX_POINT ( 'NONE', #8136 ) ;
#3677=STYLED_ITEM ( 'NONE', ( #7967 ), #10471 ) ;
#3685=AXIS2_PLACEMENT_3D ( 'NONE', #6831, #8891, #5896 ) ;
#3686=VECTOR ( 'NONE', #246, 1000.000000000000114 ) ;
#3690=DIRECTION ( 'NONE',  ( 1.000000000000000000, 0.000000000000000000, 0.000000000000000000 ) ) ;
#3700=AXIS2_PLACEMENT_3D ( 'NONE', #5726, #12787, #12922 ) ;
#3707=CIRCLE ( 'NONE', #2433, 3.000000000000000000 ) ;
#3719=EDGE_CURVE ( 'NONE', #4133, #2702, #8637, .T. ) ;
#3738=VERTEX_POINT ( 'NONE', #109 ) ;
#3764=DIRECTION ( 'NONE',  ( 1.000000000000000000, 0.000000000000000000, 0.000000000000000000 ) ) ;
#3766=CARTESIAN_POINT ( 'NONE',  ( 220.3999999999999773, 2.249562960690858038, -0.04434507737934524629 ) ) ;
#3769=EDGE_CURVE ( 'NONE', #8424, #379, #3221, .T. ) ;
#3794=CIRCLE ( 'NONE', #11251, 4.000000000000000000 ) ;
#3808=AXIS2_PLACEMENT_3D ( 'NONE', #1087, #11288, #10484 ) ;
#3815=AXIS2_PLACEMENT_3D ( 'NONE', #11376, #8446, #4488 ) ;
#3820=ORIENTED_EDGE ( 'NONE', *, *, #7611, .T. ) ;
#3825=CIRCLE ( 'NONE', #11718, 1.949999999999999734 ) ;
#3827=SURFACE_SIDE_STYLE ('',( #9828 ) ) ;
#3837=ADVANCED_FACE ( 'NONE', ( #11369 ), #1611, .F. ) ;
#3844=DIRECTION ( 'NONE',  ( 0.000000000000000000, 0.9998057603070480415, -0.01970892327970899874 ) ) ;
#3849=ADVANCED_FACE ( 'NONE', ( #5293 ), #11407, .F. ) ;
#3907=CIRCLE ( 'NONE', #8597, 2.900000000000000355 ) ;
#3915=EDGE_CURVE ( 'NONE', #6766, #3428, #5011, .T. ) ;
#3950=ORIENTED_EDGE ( 'NONE', *, *, #11328, .T. ) ;
#3954=VERTEX_POINT ( 'NONE', #3415 ) ;
#3965=ORIENTED_EDGE ( 'NONE', *, *, #2252, .T. ) ;
#3990=DIRECTION ( 'NONE',  ( 1.000000000000000000, 0.000000000000000000, 0.000000000000000000 ) ) ;
#3996=CARTESIAN_POINT ( 'NONE',  ( 229.9000000000000057, 4.038376339049584374, 2.818069648572310459 ) ) ;
#4025=ORIENTED_EDGE ( 'NONE', *, *, #2885, .F. ) ;
#4028=AXIS2_PLACEMENT_3D ( 'NONE', #8020, #887, #11013 ) ;
#4031=EDGE_CURVE ( 'NONE', #13016, #926, #7754, .T. ) ;
#4036=CARTESIAN_POINT ( 'NONE',  ( 234.3487510399341716, 0.000000000000000000, 0.000000000000000000 ) ) ;
#4037=AXIS2_PLACEMENT_3D ( 'NONE', #1322, #5388, #4502 ) ;
#4042=ORIENTED_EDGE ( 'NONE', *, *, #11276, .F. ) ;
#4063=ORIENTED_EDGE ( 'NONE', *, *, #4879, .T. ) ;
#4082=EDGE_LOOP ( 'NONE', ( #11368, #9113, #10169, #3950 ) ) ;
#4133=VERTEX_POINT ( 'NONE', #4742 ) ;
#4139=CARTESIAN_POINT ( 'NONE',  ( 227.3999999999999773, 4.550331206106116078, 2.508881407069060376 ) ) ;
#4153=VECTOR ( 'NONE', #7074, 1000.000000000000114 ) ;
#4166=AXIS2_PLACEMENT_3D ( 'NONE', #2732, #4740, #10812 ) ;
#4167=VECTOR ( 'NONE', #7202, 1000.000000000000000 ) ;
#4168=DIRECTION ( 'NONE',  ( 0.7071067811865480168, -0.7069694329824850465, 0.01393631330096772175 ) ) ;
#4207=EDGE_LOOP ( 'NONE', ( #12770, #7622, #4983, #6830 ) ) ;
#4260=DIRECTION ( 'NONE',  ( 1.000000000000000000, 0.000000000000000000, 0.000000000000000000 ) ) ;
#4293=ORIENTED_EDGE ( 'NONE', *, *, #3915, .T. ) ;
#4301=DIRECTION ( 'NONE',  ( 0.000000000000000000, -0.01970892327970899874, -0.9998057603070481525 ) ) ;
#4302=CIRCLE ( 'NONE', #2390, 3.350000000000000089 ) ;
#4316=AXIS2_PLACEMENT_3D ( 'NONE', #2729, #6820, #7615 ) ;
#4324=AXIS2_PLACEMENT_3D ( 'NONE', #8321, #12380, #2244 ) ;
#4344=VERTEX_POINT ( 'NONE', #8549 ) ;
#4361=CARTESIAN_POINT ( 'NONE',  ( 220.3999999999999773, -2.249562960690858038, 0.04434507737934551691 ) ) ;
#4363=ORIENTED_EDGE ( 'NONE', *, *, #10793, .T. ) ;
#4367=DIRECTION ( 'NONE',  ( 1.000000000000000000, 0.000000000000000000, 0.000000000000000000 ) ) ;
#4378=CARTESIAN_POINT ( 'NONE',  ( 227.3999999999999773, 0.000000000000000000, 0.000000000000000000 ) ) ;
#4396=CARTESIAN_POINT ( 'NONE',  ( 235.4000000000000057, -2.749465840844381948, 0.05419953901920007699 ) ) ;
#4417=DIRECTION ( 'NONE',  ( 0.000000000000000000, 0.8757116489157734662, 0.4828344519120573719 ) ) ;
#4473=CARTESIAN_POINT ( 'NONE',  ( 227.3999999999999773, 2.172755033604258923, -3.940702420120982374 ) ) ;
#4476=CARTESIAN_POINT ( 'NONE',  ( 227.3999999999999773, 2.326370887777457153, 3.852012265362291465 ) ) ;
#4485=ORIENTED_EDGE ( 'NONE', *, *, #7306, .T. ) ;
#4488=DIRECTION ( 'NONE',  ( 1.000000000000000000, 0.000000000000000000, 0.000000000000000000 ) ) ;
#4502=DIRECTION ( 'NONE',  ( 0.000000000000000000, 0.9998057603070481525, -0.01970892327970900221 ) ) ;
#4506=AXIS2_PLACEMENT_3D ( 'NONE', #5056, #4905, #8339 ) ;
#4508=EDGE_CURVE ( 'NONE', #13016, #5655, #5943, .T. ) ;
#4525=AXIS2_PLACEMENT_3D ( 'NONE', #5533, #6743, #10663 ) ;
#4552=DIRECTION ( 'NONE',  ( 1.000000000000000000, 0.000000000000000000, 0.000000000000000000 ) ) ;
#4555=ADVANCED_FACE ( 'NONE', ( #1065 ), #10190, .T. ) ;
#4560=( LENGTH_UNIT ( ) NAMED_UNIT ( * ) SI_UNIT ( .MILLI., .METRE. ) );
#4578=ADVANCED_FACE ( 'NONE', ( #6336 ), #7070, .F. ) ;
#4580=ADVANCED_FACE ( 'NONE', ( #3058 ), #6275, .F. ) ;
#4597=VERTEX_POINT ( 'NONE', #10389 ) ;
#4612=ORIENTED_EDGE ( 'NONE', *, *, #12838, .T. ) ;
#4626=EDGE_CURVE ( 'NONE', #12401, #379, #4302, .T. ) ;
#4650=CARTESIAN_POINT ( 'NONE',  ( 235.0999999999999943, 0.000000000000000000, 0.000000000000000000 ) ) ;
#4697=EDGE_LOOP ( 'NONE', ( #7287, #3202 ) ) ;
#4699=CARTESIAN_POINT ( 'NONE',  ( 233.5975020798683204, 2.199572672675505824, -0.04335963121535980208 ) ) ;
#4701=FACE_BOUND ( 'NONE', #9566, .T. ) ;
#4709=ORIENTED_EDGE ( 'NONE', *, *, #6048, .F. ) ;
#4713=CARTESIAN_POINT ( 'NONE',  ( 235.0999999999999943, -0.05419953901919974393, -2.749465840844381948 ) ) ;
#4732=ORIENTED_EDGE ( 'NONE', *, *, #6091, .F. ) ;
#4740=DIRECTION ( 'NONE',  ( 1.000000000000000000, 0.000000000000000000, 0.000000000000000000 ) ) ;
#4742=CARTESIAN_POINT ( 'NONE',  ( 226.1499999999999773, 1.749660080537334128, -0.03449061573949074866 ) ) ;
#4750=EDGE_LOOP ( 'NONE', ( #8295, #11011, #903, #2738, #8035 ) ) ;
#4752=DIRECTION ( 'NONE',  ( 0.000000000000000000, 0.01970892327970883220, 0.9998057603070481525 ) ) ;
#4758=VECTOR ( 'NONE', #5269, 1000.000000000000227 ) ;
#4764=ORIENTED_EDGE ( 'NONE', *, *, #4508, .F. ) ;
#4765=EDGE_CURVE ( 'NONE', #7894, #5570, #5590, .T. ) ;
#4779=VECTOR ( 'NONE', #1983, 1000.000000000000227 ) ;
#4805=CARTESIAN_POINT ( 'NONE',  ( 220.3999999999999773, 0.000000000000000000, 0.000000000000000000 ) ) ;
#4815=ORIENTED_EDGE ( 'NONE', *, *, #1603, .F. ) ;
#4816=FACE_OUTER_BOUND ( 'NONE', #2290, .T. ) ;
#4819=FILL_AREA_STYLE ('',( #7696 ) ) ;
#4826=VERTEX_POINT ( 'NONE', #6600 ) ;
#4831=CARTESIAN_POINT ( 'NONE',  ( 229.9000000000000057, -0.07883569311883599495, -3.999223041228192610 ) ) ;
#4853=DIRECTION ( 'NONE',  ( 0.000000000000000000, 0.9998057603070480415, -0.01970892327970899874 ) ) ;
#4870=LINE ( 'NONE', #809, #4153 ) ;
#4879=EDGE_CURVE ( 'NONE', #10920, #11715, #6533, .T. ) ;
#4881=DIRECTION ( 'NONE',  ( 0.000000000000000000, 0.9998057603070481525, -0.01970892327970899874 ) ) ;
#4887=PRODUCT_DEFINITION_CONTEXT ( 'detailed design', #9326, 'design' ) ;
#4897=DIRECTION ( 'NONE',  ( 0.000000000000000000, 0.9998057603070481525, -0.01970892327970899874 ) ) ;
#4905=DIRECTION ( 'NONE',  ( 1.000000000000000000, 0.000000000000000000, 0.000000000000000000 ) ) ;
#4922=CARTESIAN_POINT ( 'NONE',  ( 235.4000000000000057, 0.000000000000000000, 0.000000000000000000 ) ) ;
#4945=AXIS2_PLACEMENT_3D ( 'NONE', #10398, #9701, #8715 ) ;
#4972=CIRCLE ( 'NONE', #6691, 1.000000000000000000 ) ;
#4973=CARTESIAN_POINT ( 'NONE',  ( 220.3999999999999773, 0.000000000000000000, 0.000000000000000000 ) ) ;
#4983=ORIENTED_EDGE ( 'NONE', *, *, #775, .T. ) ;
#4994=CARTESIAN_POINT ( 'NONE',  ( 235.4000000000000057, -1.749660080537334128, 0.03449061573949095683 ) ) ;
#5000=AXIS2_PLACEMENT_3D ( 'NONE', #2992, #9010, #876 ) ;
#5011=CIRCLE ( 'NONE', #2453, 3.153020646647511249 ) ;
#5029=DIRECTION ( 'NONE',  ( 1.000000000000000000, 0.000000000000000000, 0.000000000000000000 ) ) ;
#5055=( GEOMETRIC_REPRESENTATION_CONTEXT ( 3 ) GLOBAL_UNCERTAINTY_ASSIGNED_CONTEXT ( ( #6894 ) ) GLOBAL_UNIT_ASSIGNED_CONTEXT ( ( #4560, #8640, #11577 ) ) REPRESENTATION_CONTEXT ( 'NONE', 'WORKASPACE' ) );
#5056=CARTESIAN_POINT ( 'NONE',  ( 227.3999999999999773, -0.1281080013181084831, -6.498737441995811714 ) ) ;
#5057=ORIENTED_EDGE ( 'NONE', *, *, #10070, .T. ) ;
#5058=ORIENTED_EDGE ( 'NONE', *, *, #3080, .T. ) ;
#5063=CONICAL_SURFACE ( 'NONE', #824, 2.250000000000000000, 0.4188790204786335125 ) ;
#5070=DIRECTION ( 'NONE',  ( 1.000000000000000000, 0.000000000000000000, 0.000000000000000000 ) ) ;
#5127=DIRECTION ( 'NONE',  ( -0.000000000000000000, 0.8560027256360644987, -0.5169713083949903920 ) ) ;
#5128=EDGE_CURVE ( 'NONE', #5475, #6733, #3374, .T. ) ;
#5138=ORIENTED_EDGE ( 'NONE', *, *, #14, .F. ) ;
#5143=ORIENTED_EDGE ( 'NONE', *, *, #4031, .F. ) ;
#5155=ORIENTED_EDGE ( 'NONE', *, *, #6073, .T. ) ;
#5161=DIRECTION ( 'NONE',  ( 1.000000000000000000, 0.000000000000000000, 0.000000000000000000 ) ) ;
#5172=ORIENTED_EDGE ( 'NONE', *, *, #7902, .T. ) ;
#5197=LINE ( 'NONE', #12071, #7579 ) ;
#5223=ORIENTED_EDGE ( 'NONE', *, *, #12085, .T. ) ;
#5226=VERTEX_POINT ( 'NONE', #6028 ) ;
#5229=ORIENTED_EDGE ( 'NONE', *, *, #7578, .T. ) ;
#5243=FACE_BOUND ( 'NONE', #364, .T. ) ;
#5244=ORIENTED_EDGE ( 'NONE', *, *, #278, .T. ) ;
#5256=EDGE_CURVE ( 'NONE', #9399, #6766, #7228, .T. ) ;
#5265=CARTESIAN_POINT ( 'NONE',  ( 227.3999999999999773, 2.999417280921144346, -0.05912676983912699968 ) ) ;
#5268=ADVANCED_FACE ( 'NONE', ( #2350 ), #6228, .F. ) ;
#5269=DIRECTION ( 'NONE',  ( -0.000000000000000000, 0.8560027256360644987, -0.5169713083949903920 ) ) ;
#5291=EDGE_LOOP ( 'NONE', ( #183, #12677, #7499, #2581 ) ) ;
#5293=FACE_OUTER_BOUND ( 'NONE', #8, .T. ) ;
#5299=DIRECTION ( 'NONE',  ( 0.000000000000000000, -0.8560027256360642767, 0.5169713083949908361 ) ) ;
#5303=CARTESIAN_POINT ( 'NONE',  ( 227.3999999999999773, 0.000000000000000000, 0.000000000000000000 ) ) ;
#5308=CARTESIAN_POINT ( 'NONE',  ( 233.5975020798683204, 0.000000000000000000, 0.000000000000000000 ) ) ;
#5334=DIRECTION ( 'NONE',  ( 0.000000000000000000, 0.9998057603070481525, -0.01970892327970899874 ) ) ;
#5335=CARTESIAN_POINT ( 'NONE',  ( 224.4939760857161843, -2.899436704890439476, 0.05715587751115645126 ) ) ;
#5341=CARTESIAN_POINT ( 'NONE',  ( 227.3999999999999773, -4.447920636657316074, 2.686261716586446635 ) ) ;
#5347=EDGE_CURVE ( 'NONE', #10920, #13016, #3336, .T. ) ;
#5366=VERTEX_POINT ( 'NONE', #2148 ) ;
#5367=AXIS2_PLACEMENT_3D ( 'NONE', #11739, #1470, #1663 ) ;
#5388=DIRECTION ( 'NONE',  ( 1.000000000000000000, 0.000000000000000000, 0.000000000000000000 ) ) ;
#5404=DIRECTION ( 'NONE',  ( 0.000000000000000000, 0.8757116489157734662, 0.4828344519120573719 ) ) ;
#5420=DIRECTION ( 'NONE',  ( 0.000000000000000000, 0.01970892327970883220, 0.9998057603070481525 ) ) ;
#5428=DIRECTION ( 'NONE',  ( 0.000000000000000000, 0.9998057603070481525, -0.01970892327970899874 ) ) ;
#5454=ADVANCED_FACE ( 'NONE', ( #1289 ), #5063, .T. ) ;
#5475=VERTEX_POINT ( 'NONE', #2475 ) ;
#5489=ORIENTED_EDGE ( 'NONE', *, *, #6073, .F. ) ;
#5494=EDGE_CURVE ( 'NONE', #11715, #3954, #1546, .T. ) ;
#5499=LINE ( 'NONE', #3353, #6700 ) ;
#5502=VECTOR ( 'NONE', #1139, 1000.000000000000227 ) ;
#5510=DIRECTION ( 'NONE',  ( 0.000000000000000000, 0.9998057603070480415, -0.01970892327970899874 ) ) ;
#5517=CARTESIAN_POINT ( 'NONE',  ( 220.3999999999999773, -0.9998057603070324983, 0.01970892327970881139 ) ) ;
#5533=CARTESIAN_POINT ( 'NONE',  ( 227.3999999999999773, -0.1281080013181084831, -6.498737441995811714 ) ) ;
#5553=EDGE_LOOP ( 'NONE', ( #3820, #11857 ) ) ;
#5562=DIRECTION ( 'NONE',  ( -1.000000000000000000, 0.000000000000000000, 0.000000000000000000 ) ) ;
#5570=VERTEX_POINT ( 'NONE', #12733 ) ;
#5571=DIRECTION ( 'NONE',  ( -1.000000000000000000, 0.000000000000000000, 0.000000000000000000 ) ) ;
#5572=ORIENTED_EDGE ( 'NONE', *, *, #2705, .F. ) ;
#5584=CARTESIAN_POINT ( 'NONE',  ( 220.3999999999999773, 0.000000000000000000, 0.000000000000000000 ) ) ;
#5589=ORIENTED_EDGE ( 'NONE', *, *, #12425, .T. ) ;
#5590=LINE ( 'NONE', #1400, #10834 ) ;
#5645=FACE_OUTER_BOUND ( 'NONE', #7443, .T. ) ;
#5651=DIRECTION ( 'NONE',  ( 0.000000000000000000, 0.9998057603070480415, -0.01970892327970899874 ) ) ;
#5653=AXIS2_PLACEMENT_3D ( 'NONE', #2362, #3283, #12495 ) ;
#5655=VERTEX_POINT ( 'NONE', #7742 ) ;
#5664=CARTESIAN_POINT ( 'NONE',  ( 222.0845275804282153, -1.749660080537334128, 0.03449061573949095683 ) ) ;
#5706=ADVANCED_FACE ( 'NONE', ( #12937 ), #12320, .T. ) ;
#5713=CARTESIAN_POINT ( 'NONE',  ( 235.0999999999999943, -2.749465840844381948, 0.05419953901920007699 ) ) ;
#5726=CARTESIAN_POINT ( 'NONE',  ( 235.4000000000000057, 0.000000000000000000, 0.000000000000000000 ) ) ;
#5734=EDGE_CURVE ( 'NONE', #6766, #2870, #4870, .T. ) ;
#5753=AXIS2_PLACEMENT_3D ( 'NONE', #2334, #7470, #8540 ) ;
#5758=VERTEX_POINT ( 'NONE', #7010 ) ;
#5777=CARTESIAN_POINT ( 'NONE',  ( 222.8706404512946904, 0.000000000000000000, 0.000000000000000000 ) ) ;
#5800=CIRCLE ( 'NONE', #10493, 4.500000000000000000 ) ;
#5801=LINE ( 'NONE', #2590, #3555 ) ;
#5815=EDGE_CURVE ( 'NONE', #6766, #9399, #6078, .T. ) ;
#5817=AXIS2_PLACEMENT_3D ( 'NONE', #10809, #3609, #9604 ) ;
#5821=AXIS2_PLACEMENT_3D ( 'NONE', #2356, #11493, #2283 ) ;
#5829=VECTOR ( 'NONE', #4552, 1000.000000000000000 ) ;
#5836=FACE_OUTER_BOUND ( 'NONE', #8972, .T. ) ;
#5867=ADVANCED_FACE ( 'NONE', ( #8137 ), #964, .T. ) ;
#5891=CARTESIAN_POINT ( 'NONE',  ( 220.3999999999999773, 0.9998057603070324983, -0.01970892327970869343 ) ) ;
#5896=DIRECTION ( 'NONE',  ( 0.000000000000000000, 0.9998057603070480415, -0.01970892327970899874 ) ) ;
#5902=DIRECTION ( 'NONE',  ( 1.000000000000000000, 0.000000000000000000, 0.000000000000000000 ) ) ;
#5934=DIRECTION ( 'NONE',  ( 0.000000000000000000, -0.9998057603070481525, 0.01970892327970899874 ) ) ;
#5942=AXIS2_PLACEMENT_3D ( 'NONE', #4922, #9857, #8996 ) ;
#5943=LINE ( 'NONE', #1743, #6230 ) ;
#5947=LINE ( 'NONE', #3996, #2092 ) ;
#5954=ORIENTED_EDGE ( 'NONE', *, *, #657, .F. ) ;
#5972=ORIENTED_EDGE ( 'NONE', *, *, #9889, .T. ) ;
#5990=FACE_OUTER_BOUND ( 'NONE', #6022, .T. ) ;
#6000=CARTESIAN_POINT ( 'NONE',  ( 227.3999999999999773, -0.1281080013181084831, -6.498737441995811714 ) ) ;
#6008=EDGE_CURVE ( 'NONE', #204, #3634, #541, .T. ) ;
#6022=EDGE_LOOP ( 'NONE', ( #1622, #8019, #7185, #4732, #1441 ) ) ;
#6028=CARTESIAN_POINT ( 'NONE',  ( 233.5975020798683204, -2.999417280921144346, 0.05912676983912736745 ) ) ;
#6048=EDGE_CURVE ( 'NONE', #8424, #11763, #2868, .T. ) ;
#6073=EDGE_CURVE ( 'NONE', #2870, #6308, #10553, .T. ) ;
#6078=CIRCLE ( 'NONE', #7990, 3.823498366181860231 ) ;
#6091=EDGE_CURVE ( 'NONE', #431, #8768, #8655, .T. ) ;
#6093=ORIENTED_EDGE ( 'NONE', *, *, #7611, .F. ) ;
#6094=ORIENTED_EDGE ( 'NONE', *, *, #10701, .T. ) ;
#6109=LINE ( 'NONE', #1039, #10048 ) ;
#6110=DIRECTION ( 'NONE',  ( 0.000000000000000000, 0.9998057603070480415, -0.01970892327970899874 ) ) ;
#6152=ORIENTED_EDGE ( 'NONE', *, *, #7902, .F. ) ;
#6172=ORIENTED_EDGE ( 'NONE', *, *, #3080, .F. ) ;
#6188=CARTESIAN_POINT ( 'NONE',  ( 224.4939760857161843, 6.051844909775672576, -0.1192985195352703198 ) ) ;
#6202=LINE ( 'NONE', #394, #530 ) ;
#6209=LINE ( 'NONE', #3123, #5502 ) ;
#6211=CARTESIAN_POINT ( 'NONE',  ( 233.5975020798683204, 0.000000000000000000, 0.000000000000000000 ) ) ;
#6228=CYLINDRICAL_SURFACE ( 'NONE', #9348, 3.000000000000000000 ) ;
#6230=VECTOR ( 'NONE', #10004, 1000.000000000000000 ) ;
#6238=DIRECTION ( 'NONE',  ( 0.000000000000000000, 0.9998057603070481525, -0.01970892327970900221 ) ) ;
#6239=EDGE_LOOP ( 'NONE', ( #10741, #853, #5972 ) ) ;
#6240=DIRECTION ( 'NONE',  ( 1.000000000000000000, 0.000000000000000000, 0.000000000000000000 ) ) ;
#6244=ADVANCED_FACE ( 'NONE', ( #11495 ), #9177, .F. ) ;
#6255=ORIENTED_EDGE ( 'NONE', *, *, #12085, .F. ) ;
#6275=PLANE ( 'NONE',  #4506 ) ;
#6302=VECTOR ( 'NONE', #3154, 1000.000000000000114 ) ;
#6308=VERTEX_POINT ( 'NONE', #4476 ) ;
#6314=CARTESIAN_POINT ( 'NONE',  ( 235.4000000000000057, -2.999417280921144346, 0.05912676983912699968 ) ) ;
#6336=FACE_OUTER_BOUND ( 'NONE', #1831, .T. ) ;
#6368=CARTESIAN_POINT ( 'NONE',  ( 224.4939760857161843, 0.000000000000000000, 0.000000000000000000 ) ) ;
#6372=DIRECTION ( 'NONE',  ( 0.000000000000000000, 0.9998057603070480415, -0.01970892327970899527 ) ) ;
#6378=DIRECTION ( 'NONE',  ( 1.000000000000000000, 0.000000000000000000, 0.000000000000000000 ) ) ;
#6387=DIRECTION ( 'NONE',  ( 1.000000000000000000, 0.000000000000000000, 0.000000000000000000 ) ) ;
#6400=PRODUCT_CONTEXT ( 'NONE', #9515, 'mechanical' ) ;
#6410=DIRECTION ( 'NONE',  ( -0.000000000000000000, 0.01970892327970912364, 0.9998057603070482635 ) ) ;
#6413=ADVANCED_FACE ( 'NONE', ( #10683 ), #7152, .F. ) ;
#6422=ORIENTED_EDGE ( 'NONE', *, *, #7578, .F. ) ;
#6423=DIRECTION ( 'NONE',  ( 0.000000000000000000, 0.9998057603070481525, -0.01970892327970899874 ) ) ;
#6442=CARTESIAN_POINT ( 'NONE',  ( 227.3999999999999773, 4.499125921381716076, -0.08869015475868961829 ) ) ;
#6452=( GEOMETRIC_REPRESENTATION_CONTEXT ( 3 ) GLOBAL_UNCERTAINTY_ASSIGNED_CONTEXT ( ( #9983 ) ) GLOBAL_UNIT_ASSIGNED_CONTEXT ( ( #10967, #3626, #1898 ) ) REPRESENTATION_CONTEXT ( 'NONE', 'WORKASPACE' ) );
#6456=ORIENTED_EDGE ( 'NONE', *, *, #9388, .T. ) ;
#6459=CARTESIAN_POINT ( 'NONE',  ( 235.4000000000000057, 4.447920636657316074, -2.686261716586451520 ) ) ;
#6470=CIRCLE ( 'NONE', #12842, 2.900000000000000355 ) ;
#6480=TOROIDAL_SURFACE ( 'NONE', #8185, 2.750000000000000000, 0.8000000000000000444 ) ;
#6481=DIRECTION ( 'NONE',  ( 0.000000000000000000, 0.9998057603070481525, -0.01970892327970899874 ) ) ;
#6507=ORIENTED_EDGE ( 'NONE', *, *, #2624, .T. ) ;
#6524=CARTESIAN_POINT ( 'NONE',  ( 227.3999999999999773, -0.1024105694488001289, -5.195143123655522110 ) ) ;
#6527=DIRECTION ( 'NONE',  ( 1.000000000000000000, 0.000000000000000000, 0.000000000000000000 ) ) ;
#6533=LINE ( 'NONE', #2583, #12118 ) ;
#6538=FACE_OUTER_BOUND ( 'NONE', #8239, .T. ) ;
#6544=VECTOR ( 'NONE', #3275, 1000.000000000000114 ) ;
#6554=CARTESIAN_POINT ( 'NONE',  ( 227.3999999999999773, -2.999417280921144346, 0.05912676983912736745 ) ) ;
#6559=DIRECTION ( 'NONE',  ( 0.000000000000000000, 0.9998057603070480415, -0.01970892327970899874 ) ) ;
#6572=DIRECTION ( 'NONE',  ( 0.000000000000000000, 0.9998057603070481525, -0.01970892327970899874 ) ) ;
#6586=DIRECTION ( 'NONE',  ( 1.000000000000000000, 0.000000000000000000, 0.000000000000000000 ) ) ;
#6600=CARTESIAN_POINT ( 'NONE',  ( 235.0999999999999943, 1.949621232598743648, -0.03843240039543253939 ) ) ;
#6603=DIRECTION ( 'NONE',  ( 0.000000000000000000, 0.01970892327970899874, 0.9998057603070481525 ) ) ;
#6607=DIRECTION ( 'NONE',  ( 0.000000000000000000, -0.9998057603070480415, 0.01970892327970911323 ) ) ;
#6627=DIRECTION ( 'NONE',  ( 0.000000000000000000, 0.9998057603070481525, -0.01970892327970899874 ) ) ;
#6669=ADVANCED_BREP_SHAPE_REPRESENTATION ( '', ( #10471, #805 ), #5055 ) ;
#6673=PLANE ( 'NONE',  #12640 ) ;
#6683=CIRCLE ( 'NONE', #9225, 1.750000000000000000 ) ;
#6691=AXIS2_PLACEMENT_3D ( 'NONE', #8835, #5902, #4897 ) ;
#6700=VECTOR ( 'NONE', #8318, 1000.000000000000000 ) ;
#6711=CARTESIAN_POINT ( 'NONE',  ( 0.000000000000000000, 0.000000000000000000, 0.000000000000000000 ) ) ;
#6718=ORIENTED_EDGE ( 'NONE', *, *, #5128, .F. ) ;
#6727=AXIS2_PLACEMENT_3D ( 'NONE', #11851, #586, #5651 ) ;
#6733=VERTEX_POINT ( 'NONE', #11064 ) ;
#6740=DIRECTION ( 'NONE',  ( 0.000000000000000000, 0.9998057603070480415, -0.01970892327970899874 ) ) ;
#6743=DIRECTION ( 'NONE',  ( 1.000000000000000000, 0.000000000000000000, 0.000000000000000000 ) ) ;
#6756=DIRECTION ( 'NONE',  ( 0.000000000000000000, 0.9998057603070481525, -0.01970892327970899874 ) ) ;
#6761=ORIENTED_EDGE ( 'NONE', *, *, #3769, .T. ) ;
#6766=VERTEX_POINT ( 'NONE', #7932 ) ;
#6785=PLANE ( 'NONE',  #163 ) ;
#6792=ORIENTED_EDGE ( 'NONE', *, *, #5815, .T. ) ;
#6799=PLANE ( 'NONE',  #12745 ) ;
#6811=EDGE_CURVE ( 'NONE', #4597, #2702, #6941, .T. ) ;
#6813=ORIENTED_EDGE ( 'NONE', *, *, #1353, .T. ) ;
#6820=DIRECTION ( 'NONE',  ( 1.000000000000000000, 0.000000000000000000, 0.000000000000000000 ) ) ;
#6827=EDGE_LOOP ( 'NONE', ( #1705, #12022, #6507, #10783 ) ) ;
#6830=ORIENTED_EDGE ( 'NONE', *, *, #11373, .T. ) ;
#6831=CARTESIAN_POINT ( 'NONE',  ( 220.3999999999999773, 0.000000000000000000, 0.000000000000000000 ) ) ;
#6838=VERTEX_POINT ( 'NONE', #4 ) ;
#6842=AXIS2_PLACEMENT_3D ( 'NONE', #4699, #9635, #10711 ) ;
#6848=AXIS2_PLACEMENT_3D ( 'NONE', #5777, #3764, #12975 ) ;
#6856=DIRECTION ( 'NONE',  ( 0.000000000000000000, -0.8757116489157734662, -0.4828344519120573719 ) ) ;
#6857=ORIENTED_EDGE ( 'NONE', *, *, #521, .F. ) ;
#6868=EDGE_CURVE ( 'NONE', #4826, #3738, #2444, .T. ) ;
#6882=EDGE_CURVE ( 'NONE', #1281, #3345, #6202, .T. ) ;
#6894=UNCERTAINTY_MEASURE_WITH_UNIT (LENGTH_MEASURE( 1.000000000000000082E-05 ), #4560, 'distance_accuracy_value', 'NONE');
#6901=DIRECTION ( 'NONE',  ( 0.000000000000000000, -0.01970892327970899874, -0.9998057603070481525 ) ) ;
#6925=CARTESIAN_POINT ( 'NONE',  ( 227.3999999999999773, 0.1024105694487990881, 5.195143123655512341 ) ) ;
#6941=LINE ( 'NONE', #4994, #10311 ) ;
#6968=DIRECTION ( 'NONE',  ( 0.000000000000000000, -0.9998057603070481525, 0.01970892327970912364 ) ) ;
#7005=ORIENTED_EDGE ( 'NONE', *, *, #6882, .T. ) ;
#7010=CARTESIAN_POINT ( 'NONE',  ( 229.9000000000000057, -3.999223041228192610, 0.07883569311883648068 ) ) ;
#7045=DIRECTION ( 'NONE',  ( -0.7071067811865490160, -0.7069694329824840473, 0.01393631330096761593 ) ) ;
#7049=EDGE_CURVE ( 'NONE', #6308, #7991, #788, .T. ) ;
#7059=CIRCLE ( 'NONE', #1311, 2.749999999999999556 ) ;
#7062=PLANE ( 'NONE',  #9976 ) ;
#7070=PLANE ( 'NONE',  #2174 ) ;
#7074=DIRECTION ( 'NONE',  ( 0.7071067811865480168, 0.7069694329824850465, -0.01393631330096763501 ) ) ;
#7099=EDGE_CURVE ( 'NONE', #6838, #3954, #751, .T. ) ;
#7108=ORIENTED_EDGE ( 'NONE', *, *, #11196, .T. ) ;
#7116=CARTESIAN_POINT ( 'NONE',  ( 227.3999999999999773, 4.550331206106116078, 2.508881407069060376 ) ) ;
#7128=ADVANCED_FACE ( 'NONE', ( #5990 ), #983, .T. ) ;
#7132=DIRECTION ( 'NONE',  ( -1.000000000000000000, 0.000000000000000000, 0.000000000000000000 ) ) ;
#7136=DIRECTION ( 'NONE',  ( -1.000000000000000000, 0.000000000000000000, 0.000000000000000000 ) ) ;
#7152=TOROIDAL_SURFACE ( 'NONE', #4166, 6.053020646647509828, 3.153020646647509917 ) ;
#7168=DIRECTION ( 'NONE',  ( 1.000000000000000000, 0.000000000000000000, 0.000000000000000000 ) ) ;
#7185=ORIENTED_EDGE ( 'NONE', *, *, #543, .F. ) ;
#7202=DIRECTION ( 'NONE',  ( 1.000000000000000000, 0.000000000000000000, 0.000000000000000000 ) ) ;
#7226=CARTESIAN_POINT ( 'NONE',  ( 229.9000000000000057, -4.577961614500551946, -3.910532886469501701 ) ) ;
#7228=CIRCLE ( 'NONE', #3808, 3.823498366181860231 ) ;
#7229=CIRCLE ( 'NONE', #1695, 4.000000000000000000 ) ;
#7235=AXIS2_PLACEMENT_3D ( 'NONE', #2495, #6572, #2368 ) ;
#7237=DIRECTION ( 'NONE',  ( 0.000000000000000000, 0.000000000000000000, -1.000000000000000000 ) ) ;
#7252=CARTESIAN_POINT ( 'NONE',  ( 224.4939760857161843, 2.899436704890439476, -0.05715587751115609738 ) ) ;
#7276=CARTESIAN_POINT ( 'NONE',  ( 229.9000000000000057, 3.999223041228192610, -0.07883569311883599495 ) ) ;
#7278=DIRECTION ( 'NONE',  ( 1.000000000000000000, 0.000000000000000000, 0.000000000000000000 ) ) ;
#7287=ORIENTED_EDGE ( 'NONE', *, *, #2786, .T. ) ;
#7290=ADVANCED_FACE ( 'NONE', ( #5243, #1313 ), #10370, .F. ) ;
#7303=AXIS2_PLACEMENT_3D ( 'NONE', #11948, #8816, #6559 ) ;
#7306=EDGE_CURVE ( 'NONE', #11763, #12401, #9381, .T. ) ;
#7309=CARTESIAN_POINT ( 'NONE',  ( 227.3999999999999773, 0.000000000000000000, 0.000000000000000000 ) ) ;
#7315=ORIENTED_EDGE ( 'NONE', *, *, #1735, .T. ) ;
#7322=ORIENTED_EDGE ( 'NONE', *, *, #683, .F. ) ;
#7345=CARTESIAN_POINT ( 'NONE',  ( 227.3999999999999773, 0.000000000000000000, 0.000000000000000000 ) ) ;
#7371=ORIENTED_EDGE ( 'NONE', *, *, #2724, .T. ) ;
#7376=DIRECTION ( 'NONE',  ( -0.000000000000000000, 0.01970892327970912364, 0.9998057603070482635 ) ) ;
#7387=PLANE ( 'NONE',  #10850 ) ;
#7400=CARTESIAN_POINT ( 'NONE',  ( 235.0999999999999943, 0.000000000000000000, 0.000000000000000000 ) ) ;
#7412=ORIENTED_EDGE ( 'NONE', *, *, #8940, .F. ) ;
#7422=ORIENTED_EDGE ( 'NONE', *, *, #12346, .T. ) ;
#7435=PLANE ( 'NONE',  #7235 ) ;
#7442=VECTOR ( 'NONE', #5299, 1000.000000000000227 ) ;
#7443=EDGE_LOOP ( 'NONE', ( #9694, #12100, #7572, #6094 ) ) ;
#7447=DIRECTION ( 'NONE',  ( 0.000000000000000000, 0.9998057603070480415, -0.01970892327970899874 ) ) ;
#7448=CIRCLE ( 'NONE', #9148, 1.949999999999999734 ) ;
#7457=ADVANCED_FACE ( 'NONE', ( #2628 ), #12215, .T. ) ;
#7462=CARTESIAN_POINT ( 'NONE',  ( 235.0999999999999943, 2.749465840844381948, -0.05419953901919974393 ) ) ;
#7470=DIRECTION ( 'NONE',  ( 1.000000000000000000, 0.000000000000000000, 0.000000000000000000 ) ) ;
#7472=ADVANCED_FACE ( 'NONE', ( #1634 ), #9564, .F. ) ;
#7493=CARTESIAN_POINT ( 'NONE',  ( 222.0845275804282153, 0.000000000000000000, 0.000000000000000000 ) ) ;
#7499=ORIENTED_EDGE ( 'NONE', *, *, #3915, .F. ) ;
#7511=CARTESIAN_POINT ( 'NONE',  ( 235.4000000000000057, 0.000000000000000000, 0.000000000000000000 ) ) ;
#7559=EDGE_LOOP ( 'NONE', ( #10326, #9799, #9740, #11434 ) ) ;
#7572=ORIENTED_EDGE ( 'NONE', *, *, #2530, .T. ) ;
#7577=CARTESIAN_POINT ( 'NONE',  ( 224.4939760857161843, 0.000000000000000000, 0.000000000000000000 ) ) ;
#7578=EDGE_CURVE ( 'NONE', #5226, #3634, #11367, .T. ) ;
#7579=VECTOR ( 'NONE', #1876, 1000.000000000000227 ) ;
#7591=EDGE_LOOP ( 'NONE', ( #7883, #9271 ) ) ;
#7595=DIRECTION ( 'NONE',  ( 1.000000000000000000, 0.000000000000000000, 0.000000000000000000 ) ) ;
#7609=CARTESIAN_POINT ( 'NONE',  ( 227.3999999999999773, -4.550331206106116078, -2.508881407069070590 ) ) ;
#7611=EDGE_CURVE ( 'NONE', #1691, #12854, #4972, .T. ) ;
#7615=DIRECTION ( 'NONE',  ( 0.000000000000000000, 0.9998057603070481525, -0.01970892327970900221 ) ) ;
#7622=ORIENTED_EDGE ( 'NONE', *, *, #3719, .F. ) ;
#7639=DIRECTION ( 'NONE',  ( -1.000000000000000000, 0.000000000000000000, 0.000000000000000000 ) ) ;
#7650=VECTOR ( 'NONE', #5562, 1000.000000000000000 ) ;
#7675=CARTESIAN_POINT ( 'NONE',  ( 222.8706404512946904, -3.349349297028606731, 0.06602489298702547693 ) ) ;
#7681=PRODUCT_DEFINITION_FORMATION_WITH_SPECIFIED_SOURCE ( 'ANY', '', #219, .NOT_KNOWN. ) ;
#7686=EDGE_LOOP ( 'NONE', ( #12011, #776, #9872, #6857 ) ) ;
#7687=ADVANCED_FACE ( 'NONE', ( #106 ), #6480, .T. ) ;
#7688=CIRCLE ( 'NONE', #3427, 3.000000000000000000 ) ;
#7691=CYLINDRICAL_SURFACE ( 'NONE', #1564, 4.000000000000000000 ) ;
#7696=FILL_AREA_STYLE_COLOUR ( '', #2190 ) ;
#7703=CIRCLE ( 'NONE', #1959, 2.475000000000000089 ) ;
#7717=ORIENTED_EDGE ( 'NONE', *, *, #7741, .F. ) ;
#7724=CARTESIAN_POINT ( 'NONE',  ( 227.3999999999999773, 4.550331206106116078, 2.508881407069060376 ) ) ;
#7730=VECTOR ( 'NONE', #6901, 1000.000000000000114 ) ;
#7741=EDGE_CURVE ( 'NONE', #3428, #3301, #3907, .T. ) ;
#7742=CARTESIAN_POINT ( 'NONE',  ( 227.3999999999999773, -4.447920636657316074, 2.686261716586446635 ) ) ;
#7754=LINE ( 'NONE', #10753, #1893 ) ;
#7769=CARTESIAN_POINT ( 'NONE',  ( 235.4000000000000057, 0.000000000000000000, 0.000000000000000000 ) ) ;
#7780=DIRECTION ( 'NONE',  ( 0.000000000000000000, 0.9998057603070480415, -0.01970892327970899874 ) ) ;
#7788=EDGE_LOOP ( 'NONE', ( #1122, #5244, #7371, #11748 ) ) ;
#7806=FACE_OUTER_BOUND ( 'NONE', #8790, .T. ) ;
#7815=ORIENTED_EDGE ( 'NONE', *, *, #5256, .T. ) ;
#7850=AXIS2_PLACEMENT_3D ( 'NONE', #9060, #11187, #2054 ) ;
#7856=EDGE_CURVE ( 'NONE', #8770, #6308, #9277, .T. ) ;
#7868=ORIENTED_EDGE ( 'NONE', *, *, #11443, .F. ) ;
#7883=ORIENTED_EDGE ( 'NONE', *, *, #12469, .F. ) ;
#7894=VERTEX_POINT ( 'NONE', #7276 ) ;
#7902=EDGE_CURVE ( 'NONE', #5226, #3016, #11799, .T. ) ;
#7907=VECTOR ( 'NONE', #4168, 1000.000000000000114 ) ;
#7927=VECTOR ( 'NONE', #4301, 1000.000000000000114 ) ;
#7932=CARTESIAN_POINT ( 'NONE',  ( 226.7234983661818717, 3.822755691033211001, -0.07535703595917098152 ) ) ;
#7939=ORIENTED_EDGE ( 'NONE', *, *, #2228, .F. ) ;
#7957=ORIENTED_EDGE ( 'NONE', *, *, #4626, .T. ) ;
#7961=DIRECTION ( 'NONE',  ( 1.000000000000000000, 0.000000000000000000, 0.000000000000000000 ) ) ;
#7967=PRESENTATION_STYLE_ASSIGNMENT (( #11775 ) ) ;
#7988=CARTESIAN_POINT ( 'NONE',  ( 227.3999999999999773, 0.000000000000000000, 0.000000000000000000 ) ) ;
#7990=AXIS2_PLACEMENT_3D ( 'NONE', #12070, #9935, #680 ) ;
#7991=VERTEX_POINT ( 'NONE', #4139 ) ;
#8015=CARTESIAN_POINT ( 'NONE',  ( 227.3999999999999773, -2.999417280921144346, 0.05912676983912736745 ) ) ;
#8019=ORIENTED_EDGE ( 'NONE', *, *, #11443, .T. ) ;
#8020=CARTESIAN_POINT ( 'NONE',  ( 235.4000000000000057, 0.000000000000000000, 0.000000000000000000 ) ) ;
#8035=ORIENTED_EDGE ( 'NONE', *, *, #4879, .F. ) ;
#8093=AXIS2_PLACEMENT_3D ( 'NONE', #3304, #6586, #5510 ) ;
#8102=ORIENTED_EDGE ( 'NONE', *, *, #4765, .F. ) ;
#8110=CARTESIAN_POINT ( 'NONE',  ( 226.7234983661818717, -3.822755691033211001, 0.07535703595917145337 ) ) ;
#8136=CARTESIAN_POINT ( 'NONE',  ( 234.3487510399341716, -2.474519256759935448, 0.04877958511727990831 ) ) ;
#8137=FACE_OUTER_BOUND ( 'NONE', #1153, .T. ) ;
#8146=CARTESIAN_POINT ( 'NONE',  ( 235.4000000000000057, 1.749660080537334128, -0.03449061573949074866 ) ) ;
#8157=CARTESIAN_POINT ( 'NONE',  ( 229.9000000000000057, 0.000000000000000000, 0.000000000000000000 ) ) ;
#8166=CLOSED_SHELL ( 'NONE', ( #8987, #3837, #12633, #3213, #6413, #9499, #3135, #7472, #5706, #8963, #9613, #9246, #1654, #7457, #5867, #11002, #11990, #7128, #11442, #4555, #11922, #11919, #9707, #5268, #12724, #7687, #987, #2391, #7290, #2324, #11910, #2246, #5454, #11083, #3849, #12973, #12680, #2318, #4580, #4578, #9395, #6244 ) ) ;
#8174=EDGE_CURVE ( 'NONE', #11763, #8424, #10732, .T. ) ;
#8178=CARTESIAN_POINT ( 'NONE',  ( 224.4939760857161843, 6.051844909775672576, -0.1192985195352703198 ) ) ;
#8181=LINE ( 'NONE', #8110, #7907 ) ;
#8184=DIRECTION ( 'NONE',  ( 0.000000000000000000, 0.9998057603070481525, -0.01970892327970899874 ) ) ;
#8185=AXIS2_PLACEMENT_3D ( 'NONE', #8307, #231, #6238 ) ;
#8197=AXIS2_PLACEMENT_3D ( 'NONE', #10506, #7376, #8509 ) ;
#8212=CARTESIAN_POINT ( 'NONE',  ( 235.4000000000000057, -4.550331206106116078, -2.508881407069070590 ) ) ;
#8214=EDGE_LOOP ( 'NONE', ( #6152, #5229, #2176, #11885 ) ) ;
#8233=CARTESIAN_POINT ( 'NONE',  ( 235.4000000000000057, 2.999417280921144346, -0.05912676983912663192 ) ) ;
#8239=EDGE_LOOP ( 'NONE', ( #2044, #2030, #10464, #8871, #6255 ) ) ;
#8243=ORIENTED_EDGE ( 'NONE', *, *, #8350, .F. ) ;
#8271=EDGE_CURVE ( 'NONE', #2842, #7991, #5499, .T. ) ;
#8273=EDGE_CURVE ( 'NONE', #9399, #3301, #2218, .T. ) ;
#8276=ORIENTED_EDGE ( 'NONE', *, *, #5734, .T. ) ;
#8294=ORIENTED_EDGE ( 'NONE', *, *, #7099, .T. ) ;
#8295=ORIENTED_EDGE ( 'NONE', *, *, #5347, .T. ) ;
#8301=CARTESIAN_POINT ( 'NONE',  ( 235.4000000000000057, -2.749465840844381948, 0.05419953901920007699 ) ) ;
#8307=CARTESIAN_POINT ( 'NONE',  ( 235.0999999999999943, 0.000000000000000000, 0.000000000000000000 ) ) ;
#8311=ORIENTED_EDGE ( 'NONE', *, *, #683, .T. ) ;
#8318=DIRECTION ( 'NONE',  ( -1.000000000000000000, 0.000000000000000000, 0.000000000000000000 ) ) ;
#8321=CARTESIAN_POINT ( 'NONE',  ( 235.4000000000000057, -0.05419953901919974393, -2.749465840844381948 ) ) ;
#8339=DIRECTION ( 'NONE',  ( 0.000000000000000000, 0.9998057603070481525, -0.01970892327970899874 ) ) ;
#8350=EDGE_CURVE ( 'NONE', #12027, #2438, #3707, .T. ) ;
#8356=EDGE_LOOP ( 'NONE', ( #7005, #12544, #1053 ) ) ;
#8362=LINE ( 'NONE', #6554, #6544 ) ;
#8379=DIRECTION ( 'NONE',  ( 1.000000000000000000, 0.000000000000000000, 0.000000000000000000 ) ) ;
#8412=DIRECTION ( 'NONE',  ( 1.000000000000000000, 0.000000000000000000, 0.000000000000000000 ) ) ;
#8424=VERTEX_POINT ( 'NONE', #2561 ) ;
#8445=CARTESIAN_POINT ( 'NONE',  ( 229.9000000000000057, -0.6143654365053307087, -4.885954882152276468 ) ) ;
#8446=DIRECTION ( 'NONE',  ( 0.000000000000000000, -0.4828344519120574274, 0.8757116489157735773 ) ) ;
#8461=ORIENTED_EDGE ( 'NONE', *, *, #4031, .T. ) ;
#8477=DIRECTION ( 'NONE',  ( 1.000000000000000000, 0.000000000000000000, 0.000000000000000000 ) ) ;
#8499=CIRCLE ( 'NONE', #5942, 3.000000000000000000 ) ;
#8503=ORIENTED_EDGE ( 'NONE', *, *, #10701, .F. ) ;
#8509=DIRECTION ( 'NONE',  ( 0.000000000000000000, -0.9998057603070480415, 0.01970892327970911323 ) ) ;
#8523=DIRECTION ( 'NONE',  ( -1.000000000000000000, 0.000000000000000000, 0.000000000000000000 ) ) ;
#8540=DIRECTION ( 'NONE',  ( 0.000000000000000000, 0.9998057603070480415, -0.01970892327970899874 ) ) ;
#8549=CARTESIAN_POINT ( 'NONE',  ( 235.4000000000000057, 2.749465840844381948, -0.05419953901919974393 ) ) ;
#8557=CARTESIAN_POINT ( 'NONE',  ( 227.3999999999999773, 0.1024105694487990187, 5.195143123655512341 ) ) ;
#8560=DIRECTION ( 'NONE',  ( 1.000000000000000000, 0.000000000000000000, 0.000000000000000000 ) ) ;
#8561=CONICAL_SURFACE ( 'NONE', #5367, 3.823498366181860231, 0.7853981633974476129 ) ;
#8572=PLANE ( 'NONE',  #3815 ) ;
#8580=DIRECTION ( 'NONE',  ( 1.000000000000000000, 0.000000000000000000, 0.000000000000000000 ) ) ;
#8581=AXIS2_PLACEMENT_3D ( 'NONE', #4805, #12940, #6756 ) ;
#8597=AXIS2_PLACEMENT_3D ( 'NONE', #6368, #10424, #7237 ) ;
#8608=AXIS2_PLACEMENT_3D ( 'NONE', #4973, #10043, #6110 ) ;
#8637=CIRCLE ( 'NONE', #12674, 1.750000000000000000 ) ;
#8640=( NAMED_UNIT ( * ) PLANE_ANGLE_UNIT ( ) SI_UNIT ( $, .RADIAN. ) );
#8655=LINE ( 'NONE', #11659, #10327 ) ;
#8657=ORIENTED_EDGE ( 'NONE', *, *, #6048, .T. ) ;
#8659=ORIENTED_EDGE ( 'NONE', *, *, #1603, .T. ) ;
#8666=EDGE_CURVE ( 'NONE', #3345, #11715, #12550, .T. ) ;
#8700=ORIENTED_EDGE ( 'NONE', *, *, #7099, .F. ) ;
#8707=VECTOR ( 'NONE', #10658, 1000.000000000000000 ) ;
#8715=DIRECTION ( 'NONE',  ( 0.000000000000000000, 0.9998057603070481525, -0.01970892327970899874 ) ) ;
#8724=CIRCLE ( 'NONE', #34, 4.000000000000000000 ) ;
#8732=AXIS2_PLACEMENT_3D ( 'NONE', #11608, #6410, #6607 ) ;
#8744=CARTESIAN_POINT ( 'NONE',  ( 227.3999999999999773, 4.447920636657316074, -2.686261716586451520 ) ) ;
#8755=VERTEX_POINT ( 'NONE', #8301 ) ;
#8759=CARTESIAN_POINT ( 'NONE',  ( 227.3999999999999773, -4.550331206106116078, -2.508881407069070590 ) ) ;
#8762=CARTESIAN_POINT ( 'NONE',  ( 235.4000000000000057, 0.1024105694487990881, 5.195143123655512341 ) ) ;
#8768=VERTEX_POINT ( 'NONE', #4473 ) ;
#8770=VERTEX_POINT ( 'NONE', #8557 ) ;
#8790=EDGE_LOOP ( 'NONE', ( #4293, #10573, #2130, #2064 ) ) ;
#8796=FACE_OUTER_BOUND ( 'NONE', #10999, .T. ) ;
#8816=DIRECTION ( 'NONE',  ( 1.000000000000000000, 0.000000000000000000, 0.000000000000000000 ) ) ;
#8835=CARTESIAN_POINT ( 'NONE',  ( 220.3999999999999773, 0.000000000000000000, 0.000000000000000000 ) ) ;
#8859=ORIENTED_EDGE ( 'NONE', *, *, #9731, .F. ) ;
#8865=CARTESIAN_POINT ( 'NONE',  ( 235.4000000000000057, 0.000000000000000000, 0.000000000000000000 ) ) ;
#8871=ORIENTED_EDGE ( 'NONE', *, *, #7856, .F. ) ;
#8891=DIRECTION ( 'NONE',  ( 1.000000000000000000, 0.000000000000000000, 0.000000000000000000 ) ) ;
#8934=EDGE_CURVE ( 'NONE', #12854, #1691, #9004, .T. ) ;
#8940=EDGE_CURVE ( 'NONE', #3345, #8768, #10502, .T. ) ;
#8954=CYLINDRICAL_SURFACE ( 'NONE', #4028, 1.750000000000000000 ) ;
#8958=ORIENTED_EDGE ( 'NONE', *, *, #2934, .T. ) ;
#8959=CARTESIAN_POINT ( 'NONE',  ( 235.0999999999999943, 0.000000000000000000, 0.000000000000000000 ) ) ;
#8963=ADVANCED_FACE ( 'NONE', ( #12683 ), #3245, .F. ) ;
#8972=EDGE_LOOP ( 'NONE', ( #7315, #11569, #8311, #8102 ) ) ;
#8987=ADVANCED_FACE ( 'NONE', ( #7806 ), #9224, .F. ) ;
#8996=DIRECTION ( 'NONE',  ( 0.000000000000000000, -0.9998057603070481525, 0.01970892327970899874 ) ) ;
#9004=CIRCLE ( 'NONE', #8581, 1.000000000000000000 ) ;
#9010=DIRECTION ( 'NONE',  ( 1.000000000000000000, 0.000000000000000000, 0.000000000000000000 ) ) ;
#9057=EDGE_LOOP ( 'NONE', ( #13028, #9777, #9451 ) ) ;
#9060=CARTESIAN_POINT ( 'NONE',  ( 227.3999999999999773, 0.000000000000000000, 0.000000000000000000 ) ) ;
#9105=DIRECTION ( 'NONE',  ( 1.000000000000000000, 0.000000000000000000, 0.000000000000000000 ) ) ;
#9113=ORIENTED_EDGE ( 'NONE', *, *, #11373, .F. ) ;
#9121=FACE_OUTER_BOUND ( 'NONE', #3089, .T. ) ;
#9130=VECTOR ( 'NONE', #1660, 1000.000000000000114 ) ;
#9134=VERTEX_POINT ( 'NONE', #8015 ) ;
#9148=AXIS2_PLACEMENT_3D ( 'NONE', #7400, #10133, #9276 ) ;
#9166=DIRECTION ( 'NONE',  ( 0.000000000000000000, 0.9998057603070480415, -0.01970892327970899874 ) ) ;
#9167=ORIENTED_EDGE ( 'NONE', *, *, #10184, .T. ) ;
#9177=PLANE ( 'NONE',  #2659 ) ;
#9184=AXIS2_PLACEMENT_3D ( 'NONE', #7577, #6387, #12512 ) ;
#9192=CARTESIAN_POINT ( 'NONE',  ( 229.9000000000000057, -0.1024105694488001289, -5.195143123655522110 ) ) ;
#9204=CARTESIAN_POINT ( 'NONE',  ( 234.4000000000000057, 0.000000000000000000, 0.000000000000000000 ) ) ;
#9218=EDGE_CURVE ( 'NONE', #6838, #8770, #12534, .T. ) ;
#9221=CARTESIAN_POINT ( 'NONE',  ( 220.3999999999999773, 0.000000000000000000, 0.000000000000000000 ) ) ;
#9224=TOROIDAL_SURFACE ( 'NONE', #4316, 6.053020646647509828, 3.153020646647509917 ) ;
#9225=AXIS2_PLACEMENT_3D ( 'NONE', #7493, #8560, #9607 ) ;
#9235=AXIS2_PLACEMENT_3D ( 'NONE', #2768, #10047, #6856 ) ;
#9242=FACE_OUTER_BOUND ( 'NONE', #4207, .T. ) ;
#9246=ADVANCED_FACE ( 'NONE', ( #9528 ), #12382, .F. ) ;
#9261=DIRECTION ( 'NONE',  ( 0.000000000000000000, 0.9998057603070481525, -0.01970892327970899874 ) ) ;
#9271=ORIENTED_EDGE ( 'NONE', *, *, #12346, .F. ) ;
#9276=DIRECTION ( 'NONE',  ( 0.000000000000000000, 0.9998057603070481525, -0.01970892327970900221 ) ) ;
#9277=LINE ( 'NONE', #11470, #4758 ) ;
#9326=APPLICATION_CONTEXT ( 'automotive_design' ) ;
#9348=AXIS2_PLACEMENT_3D ( 'NONE', #12358, #12287, #6423 ) ;
#9353=ORIENTED_EDGE ( 'NONE', *, *, #10793, .F. ) ;
#9354=ORIENTED_EDGE ( 'NONE', *, *, #12469, .T. ) ;
#9375=DIRECTION ( 'NONE',  ( 0.000000000000000000, 0.9998057603070480415, -0.01970892327970899874 ) ) ;
#9381=LINE ( 'NONE', #56, #3686 ) ;
#9388=EDGE_CURVE ( 'NONE', #5475, #8755, #347, .T. ) ;
#9395=ADVANCED_FACE ( 'NONE', ( #12725 ), #3461, .F. ) ;
#9399=VERTEX_POINT ( 'NONE', #2468 ) ;
#9417=AXIS2_PLACEMENT_3D ( 'NONE', #2964, #10161, #6627 ) ;
#9423=DIRECTION ( 'NONE',  ( 1.000000000000000000, 0.000000000000000000, 0.000000000000000000 ) ) ;
#9438=VECTOR ( 'NONE', #1211, 1000.000000000000227 ) ;
#9442=DIRECTION ( 'NONE',  ( 0.000000000000000000, 0.9998057603070481525, -0.01970892327970899874 ) ) ;
#9446=CONICAL_SURFACE ( 'NONE', #3685, 2.250000000000000000, 0.4188790204786335125 ) ;
#9448=ORIENTED_EDGE ( 'NONE', *, *, #11328, .F. ) ;
#9451=ORIENTED_EDGE ( 'NONE', *, *, #11276, .T. ) ;
#9464=DIRECTION ( 'NONE',  ( 0.000000000000000000, -0.8560027256360642767, 0.5169713083949908361 ) ) ;
#9497=ORIENTED_EDGE ( 'NONE', *, *, #12557, .F. ) ;
#9499=ADVANCED_FACE ( 'NONE', ( #2713 ), #8561, .T. ) ;
#9515=APPLICATION_CONTEXT ( 'automotive_design' ) ;
#9519=DIRECTION ( 'NONE',  ( 1.000000000000000000, 0.000000000000000000, 0.000000000000000000 ) ) ;
#9528=FACE_OUTER_BOUND ( 'NONE', #7788, .T. ) ;
#9564=CYLINDRICAL_SURFACE ( 'NONE', #11580, 2.749999999999999556 ) ;
#9566=EDGE_LOOP ( 'NONE', ( #9952, #467 ) ) ;
#9571=VECTOR ( 'NONE', #344, 1000.000000000000114 ) ;
#9599=ORIENTED_EDGE ( 'NONE', *, *, #6008, .F. ) ;
#9604=DIRECTION ( 'NONE',  ( 0.000000000000000000, 0.9998057603070480415, -0.01970892327970899874 ) ) ;
#9607=DIRECTION ( 'NONE',  ( 0.000000000000000000, 0.9998057603070480415, -0.01970892327970899874 ) ) ;
#9608=CONICAL_SURFACE ( 'NONE', #11758, 3.000000000000000000, 0.7853981633974490562 ) ;
#9613=ADVANCED_FACE ( 'NONE', ( #11309 ), #11173, .F. ) ;
#9619=LINE ( 'NONE', #10503, #5829 ) ;
#9628=DIRECTION ( 'NONE',  ( 0.000000000000000000, -0.9998057603070481525, 0.01970892327970899874 ) ) ;
#9635=DIRECTION ( 'NONE',  ( 0.000000000000000000, -0.01970892327970900221, -0.9998057603070482635 ) ) ;
#9641=EDGE_CURVE ( 'NONE', #12027, #1246, #6109, .T. ) ;
#9642=CIRCLE ( 'NONE', #5821, 2.749999999999999556 ) ;
#9685=AXIS2_PLACEMENT_3D ( 'NONE', #5713, #1590, #10779 ) ;
#9694=ORIENTED_EDGE ( 'NONE', *, *, #9388, .F. ) ;
#9701=DIRECTION ( 'NONE',  ( 1.000000000000000000, 0.000000000000000000, 0.000000000000000000 ) ) ;
#9707=ADVANCED_FACE ( 'NONE', ( #9242 ), #9608, .F. ) ;
#9731=EDGE_CURVE ( 'NONE', #3634, #3738, #7703, .T. ) ;
#9740=ORIENTED_EDGE ( 'NONE', *, *, #521, .T. ) ;
#9754=VECTOR ( 'NONE', #11121, 1000.000000000000000 ) ;
#9777=ORIENTED_EDGE ( 'NONE', *, *, #2228, .T. ) ;
#9786=DIRECTION ( 'NONE',  ( 1.000000000000000000, 0.000000000000000000, 0.000000000000000000 ) ) ;
#9799=ORIENTED_EDGE ( 'NONE', *, *, #10671, .F. ) ;
#9821=DIRECTION ( 'NONE',  ( 1.000000000000000000, 0.000000000000000000, 0.000000000000000000 ) ) ;
#9828=SURFACE_STYLE_FILL_AREA ( #4819 ) ;
#9836=LINE ( 'NONE', #2633, #10888 ) ;
#9844=VECTOR ( 'NONE', #11491, 1000.000000000000227 ) ;
#9857=DIRECTION ( 'NONE',  ( 1.000000000000000000, 0.000000000000000000, 0.000000000000000000 ) ) ;
#9860=CARTESIAN_POINT ( 'NONE',  ( 222.0845275804282153, 0.000000000000000000, 0.000000000000000000 ) ) ;
#9862=DIRECTION ( 'NONE',  ( 1.000000000000000000, 0.000000000000000000, 0.000000000000000000 ) ) ;
#9866=AXIS2_PLACEMENT_3D ( 'NONE', #236, #8379, #12438 ) ;
#9872=ORIENTED_EDGE ( 'NONE', *, *, #12541, .T. ) ;
#9889=EDGE_CURVE ( 'NONE', #6308, #6838, #5800, .T. ) ;
#9893=DIRECTION ( 'NONE',  ( 0.000000000000000000, 0.9998057603070481525, -0.01970892327970899874 ) ) ;
#9895=AXIS2_PLACEMENT_3D ( 'NONE', #7988, #11916, #3844 ) ;
#9926=DIRECTION ( 'NONE',  ( 1.000000000000000000, 0.000000000000000000, 0.000000000000000000 ) ) ;
#9927=CARTESIAN_POINT ( 'NONE',  ( 229.9000000000000057, -4.447920636657316074, 2.686261716586446635 ) ) ;
#9935=DIRECTION ( 'NONE',  ( 1.000000000000000000, 0.000000000000000000, 0.000000000000000000 ) ) ;
#9944=ORIENTED_EDGE ( 'NONE', *, *, #9889, .F. ) ;
#9952=ORIENTED_EDGE ( 'NONE', *, *, #1735, .F. ) ;
#9976=AXIS2_PLACEMENT_3D ( 'NONE', #12390, #3244, #7132 ) ;
#9983=UNCERTAINTY_MEASURE_WITH_UNIT (LENGTH_MEASURE( 1.000000000000000082E-05 ), #10967, 'distance_accuracy_value', 'NONE');
#10004=DIRECTION ( 'NONE',  ( -1.000000000000000000, 0.000000000000000000, 0.000000000000000000 ) ) ;
#10043=DIRECTION ( 'NONE',  ( 1.000000000000000000, 0.000000000000000000, 0.000000000000000000 ) ) ;
#10047=DIRECTION ( 'NONE',  ( -0.000000000000000000, 0.4828344519120574274, -0.8757116489157735773 ) ) ;
#10048=VECTOR ( 'NONE', #7045, 1000.000000000000114 ) ;
#10058=CARTESIAN_POINT ( 'NONE',  ( 233.5975020798683204, 0.000000000000000000, 0.000000000000000000 ) ) ;
#10070=EDGE_CURVE ( 'NONE', #5758, #7894, #1337, .T. ) ;
#10101=DIRECTION ( 'NONE',  ( 0.000000000000000000, 0.9998057603070481525, -0.01970892327970899874 ) ) ;
#10133=DIRECTION ( 'NONE',  ( 1.000000000000000000, 0.000000000000000000, 0.000000000000000000 ) ) ;
#10158=CARTESIAN_POINT ( 'NONE',  ( 227.3999999999999773, 0.000000000000000000, 0.000000000000000000 ) ) ;
#10161=DIRECTION ( 'NONE',  ( 1.000000000000000000, 0.000000000000000000, 0.000000000000000000 ) ) ;
#10169=ORIENTED_EDGE ( 'NONE', *, *, #2885, .T. ) ;
#10173=ORIENTED_EDGE ( 'NONE', *, *, #8174, .T. ) ;
#10179=LINE ( 'NONE', #2118, #9754 ) ;
#10184=EDGE_CURVE ( 'NONE', #7991, #2870, #2173, .T. ) ;
#10190=PLANE ( 'NONE',  #3231 ) ;
#10214=DIRECTION ( 'NONE',  ( -0.7071067811865490160, 0.7069694329824840473, -0.01393631330096752920 ) ) ;
#10226=AXIS2_PLACEMENT_3D ( 'NONE', #4378, #3434, #7447 ) ;
#10239=CIRCLE ( 'NONE', #6842, 0.8000000000000003775 ) ;
#10241=ORIENTED_EDGE ( 'NONE', *, *, #6868, .T. ) ;
#10278=ORIENTED_EDGE ( 'NONE', *, *, #12838, .F. ) ;
#10311=VECTOR ( 'NONE', #3990, 1000.000000000000000 ) ;
#10326=ORIENTED_EDGE ( 'NONE', *, *, #6811, .F. ) ;
#10327=VECTOR ( 'NONE', #2513, 1000.000000000000227 ) ;
#10353=EDGE_LOOP ( 'NONE', ( #10411, #5589, #8958, #9353 ) ) ;
#10370=PLANE ( 'NONE',  #4324 ) ;
#10389=CARTESIAN_POINT ( 'NONE',  ( 222.0845275804282153, -1.749660080537334572, 0.03449061573949096376 ) ) ;
#10398=CARTESIAN_POINT ( 'NONE',  ( 229.9000000000000057, 0.000000000000000000, 0.000000000000000000 ) ) ;
#10411=ORIENTED_EDGE ( 'NONE', *, *, #8934, .F. ) ;
#10424=DIRECTION ( 'NONE',  ( 1.000000000000000000, 0.000000000000000000, 0.000000000000000000 ) ) ;
#10442=EDGE_LOOP ( 'NONE', ( #9354, #628, #10278, #11317 ) ) ;
#10458=SHAPE_DEFINITION_REPRESENTATION ( #11798, #12521 ) ;
#10464=ORIENTED_EDGE ( 'NONE', *, *, #7049, .F. ) ;
#10470=LINE ( 'NONE', #1338, #12771 ) ;
#10471=MANIFOLD_SOLID_BREP ( 'NONE', #8166 ) ;
#10484=DIRECTION ( 'NONE',  ( 0.000000000000000000, 0.9998057603070481525, -0.01970892327970899874 ) ) ;
#10493=AXIS2_PLACEMENT_3D ( 'NONE', #5303, #1436, #9375 ) ;
#10495=CARTESIAN_POINT ( 'NONE',  ( 227.3999999999999773, -0.1281080013181084831, -6.498737441995811714 ) ) ;
#10502=CIRCLE ( 'NONE', #5817, 4.500000000000000000 ) ;
#10503=CARTESIAN_POINT ( 'NONE',  ( 235.4000000000000057, 2.999417280921144346, -0.05912676983912699968 ) ) ;
#10506=CARTESIAN_POINT ( 'NONE',  ( 224.4939760857161843, -6.051844909775672576, 0.1192985195352710553 ) ) ;
#10518=LINE ( 'NONE', #6459, #1702 ) ;
#10532=LINE ( 'NONE', #5265, #1371 ) ;
#10553=CIRCLE ( 'NONE', #6727, 4.500000000000000000 ) ;
#10571=ORIENTED_EDGE ( 'NONE', *, *, #3452, .T. ) ;
#10573=ORIENTED_EDGE ( 'NONE', *, *, #7741, .T. ) ;
#10591=DIRECTION ( 'NONE',  ( -0.000000000000000000, 0.5169713083949905030, 0.8560027256360646097 ) ) ;
#10635=DIRECTION ( 'NONE',  ( 1.000000000000000000, 0.000000000000000000, 0.000000000000000000 ) ) ;
#10644=CARTESIAN_POINT ( 'NONE',  ( 227.3999999999999773, -0.1281080013181084831, -6.498737441995811714 ) ) ;
#10658=DIRECTION ( 'NONE',  ( 1.000000000000000000, 0.000000000000000000, 0.000000000000000000 ) ) ;
#10659=PLANE ( 'NONE',  #932 ) ;
#10663=DIRECTION ( 'NONE',  ( 0.000000000000000000, 0.9998057603070481525, -0.01970892327970899874 ) ) ;
#10671=EDGE_CURVE ( 'NONE', #5366, #4597, #6683, .T. ) ;
#10683=FACE_OUTER_BOUND ( 'NONE', #6827, .T. ) ;
#10686=EDGE_LOOP ( 'NONE', ( #807, #4709 ) ) ;
#10701=EDGE_CURVE ( 'NONE', #4344, #8755, #9642, .T. ) ;
#10711=DIRECTION ( 'NONE',  ( 0.000000000000000000, 0.9998057603070481525, -0.01970892327970899527 ) ) ;
#10714=DIRECTION ( 'NONE',  ( 1.000000000000000000, 0.000000000000000000, 0.000000000000000000 ) ) ;
#10730=DIRECTION ( 'NONE',  ( 1.000000000000000000, 0.000000000000000000, 0.000000000000000000 ) ) ;
#10732=CIRCLE ( 'NONE', #8608, 2.250000000000000000 ) ;
#10741=ORIENTED_EDGE ( 'NONE', *, *, #9218, .T. ) ;
#10753=CARTESIAN_POINT ( 'NONE',  ( 229.9000000000000057, -3.924178331435803635, 2.975033516296866853 ) ) ;
#10765=DIRECTION ( 'NONE',  ( 0.000000000000000000, 0.000000000000000000, 1.000000000000000000 ) ) ;
#10779=DIRECTION ( 'NONE',  ( 0.000000000000000000, -0.9998057603070480415, 0.01970892327970912364 ) ) ;
#10783=ORIENTED_EDGE ( 'NONE', *, *, #3452, .F. ) ;
#10793=EDGE_CURVE ( 'NONE', #1691, #5366, #12811, .T. ) ;
#10809=CARTESIAN_POINT ( 'NONE',  ( 227.3999999999999773, 0.000000000000000000, 0.000000000000000000 ) ) ;
#10812=DIRECTION ( 'NONE',  ( 0.000000000000000000, 0.9998057603070481525, -0.01970892327970900221 ) ) ;
#10821=LINE ( 'NONE', #10891, #7730 ) ;
#10824=DIRECTION ( 'NONE',  ( 1.000000000000000000, 0.000000000000000000, 0.000000000000000000 ) ) ;
#10834=VECTOR ( 'NONE', #9519, 1000.000000000000000 ) ;
#10850=AXIS2_PLACEMENT_3D ( 'NONE', #10644, #11454, #2571 ) ;
#10888=VECTOR ( 'NONE', #2891, 1000.000000000000000 ) ;
#10891=CARTESIAN_POINT ( 'NONE',  ( 229.9000000000000057, 4.420290228262880206, -4.087913195986883075 ) ) ;
#10901=ORIENTED_EDGE ( 'NONE', *, *, #10184, .F. ) ;
#10914=ORIENTED_EDGE ( 'NONE', *, *, #1074, .F. ) ;
#10920=VERTEX_POINT ( 'NONE', #11950 ) ;
#10924=FACE_OUTER_BOUND ( 'NONE', #4697, .T. ) ;
#10944=AXIS2_PLACEMENT_3D ( 'NONE', #6211, #8412, #12276 ) ;
#10965=AXIS2_PLACEMENT_3D ( 'NONE', #8865, #7136, #5934 ) ;
#10967=( LENGTH_UNIT ( ) NAMED_UNIT ( * ) SI_UNIT ( .MILLI., .METRE. ) );
#10999=EDGE_LOOP ( 'NONE', ( #9167, #5155, #1597 ) ) ;
#11002=ADVANCED_FACE ( 'NONE', ( #6538 ), #10659, .T. ) ;
#11011=ORIENTED_EDGE ( 'NONE', *, *, #4508, .T. ) ;
#11012=PRODUCT_DEFINITION ( 'UNKNOWN', '', #7681, #4887 ) ;
#11013=DIRECTION ( 'NONE',  ( 0.000000000000000000, 0.9998057603070480415, -0.01970892327970899874 ) ) ;
#11058=DIRECTION ( 'NONE',  ( 1.000000000000000000, 0.000000000000000000, 0.000000000000000000 ) ) ;
#11064=CARTESIAN_POINT ( 'NONE',  ( 235.0999999999999943, 2.749465840844381948, -0.05419953901919974393 ) ) ;
#11078=CIRCLE ( 'NONE', #10226, 4.500000000000000000 ) ;
#11083=ADVANCED_FACE ( 'NONE', ( #11734, #11543 ), #6673, .F. ) ;
#11112=ORIENTED_EDGE ( 'NONE', *, *, #5494, .T. ) ;
#11121=DIRECTION ( 'NONE',  ( -1.000000000000000000, 0.000000000000000000, 0.000000000000000000 ) ) ;
#11133=DIRECTION ( 'NONE',  ( 0.000000000000000000, 0.9998057603070480415, -0.01970892327970899874 ) ) ;
#11135=EDGE_LOOP ( 'NONE', ( #5572, #7815, #8276, #7939, #7412, #2920 ) ) ;
#11140=VECTOR ( 'NONE', #4752, 1000.000000000000114 ) ;
#11173=CYLINDRICAL_SURFACE ( 'NONE', #9417, 3.000000000000000000 ) ;
#11187=DIRECTION ( 'NONE',  ( 1.000000000000000000, 0.000000000000000000, 0.000000000000000000 ) ) ;
#11196=EDGE_CURVE ( 'NONE', #2438, #12027, #8499, .T. ) ;
#11226=EDGE_LOOP ( 'NONE', ( #11296, #838, #5172, #4025 ) ) ;
#11230=CARTESIAN_POINT ( 'NONE',  ( 235.0999999999999943, 0.000000000000000000, 0.000000000000000000 ) ) ;
#11242=DIRECTION ( 'NONE',  ( 0.000000000000000000, -0.01970892327970900221, -0.9998057603070482635 ) ) ;
#11251=AXIS2_PLACEMENT_3D ( 'NONE', #9204, #12013, #2008 ) ;
#11276=EDGE_CURVE ( 'NONE', #2870, #431, #1800, .T. ) ;
#11288=DIRECTION ( 'NONE',  ( 1.000000000000000000, 0.000000000000000000, 0.000000000000000000 ) ) ;
#11296=ORIENTED_EDGE ( 'NONE', *, *, #2724, .F. ) ;
#11309=FACE_OUTER_BOUND ( 'NONE', #11226, .T. ) ;
#11317=ORIENTED_EDGE ( 'NONE', *, *, #6868, .F. ) ;
#11328=EDGE_CURVE ( 'NONE', #3016, #5226, #615, .T. ) ;
#11333=DIRECTION ( 'NONE',  ( 1.000000000000000000, 0.000000000000000000, 0.000000000000000000 ) ) ;
#11352=EDGE_LOOP ( 'NONE', ( #8461, #5223, #172, #1150, #4764 ) ) ;
#11357=VECTOR ( 'NONE', #8477, 1000.000000000000000 ) ;
#11367=CIRCLE ( 'NONE', #12645, 0.8000000000000003775 ) ;
#11368=ORIENTED_EDGE ( 'NONE', *, *, #13038, .F. ) ;
#11369=FACE_OUTER_BOUND ( 'NONE', #5291, .T. ) ;
#11373=EDGE_CURVE ( 'NONE', #3138, #9134, #12533, .T. ) ;
#11376=CARTESIAN_POINT ( 'NONE',  ( 235.4000000000000057, -4.447920636657316074, 2.686261716586446635 ) ) ;
#11402=DIRECTION ( 'NONE',  ( 0.000000000000000000, 0.01970892327970883220, 0.9998057603070481525 ) ) ;
#11407=CONICAL_SURFACE ( 'NONE', #5653, 1.750000000000000000, 0.4188790204786330129 ) ;
#11434=ORIENTED_EDGE ( 'NONE', *, *, #3719, .T. ) ;
#11442=ADVANCED_FACE ( 'NONE', ( #9121 ), #7062, .T. ) ;
#11443=EDGE_CURVE ( 'NONE', #11485, #1281, #10179, .T. ) ;
#11454=DIRECTION ( 'NONE',  ( 1.000000000000000000, 0.000000000000000000, 0.000000000000000000 ) ) ;
#11461=DIRECTION ( 'NONE',  ( 0.000000000000000000, 0.9998057603070480415, -0.01970892327970899874 ) ) ;
#11470=CARTESIAN_POINT ( 'NONE',  ( 227.3999999999999773, 0.1024105694487990881, 5.195143123655512341 ) ) ;
#11485=VERTEX_POINT ( 'NONE', #9192 ) ;
#11491=DIRECTION ( 'NONE',  ( 0.000000000000000000, -0.8560027256360642767, 0.5169713083949908361 ) ) ;
#11493=DIRECTION ( 'NONE',  ( 1.000000000000000000, 0.000000000000000000, 0.000000000000000000 ) ) ;
#11495=FACE_OUTER_BOUND ( 'NONE', #6239, .T. ) ;
#11500=AXIS2_PLACEMENT_3D ( 'NONE', #12646, #1387, #3437 ) ;
#11508=CYLINDRICAL_SURFACE ( 'NONE', #2541, 1.750000000000000000 ) ;
#11517=EDGE_LOOP ( 'NONE', ( #1873, #8294, #1315 ) ) ;
#11524=ORIENTED_EDGE ( 'NONE', *, *, #5734, .F. ) ;
#11526=CARTESIAN_POINT ( 'NONE',  ( 235.4000000000000057, 2.999417280921144346, -0.05912676983912663192 ) ) ;
#11543=FACE_OUTER_BOUND ( 'NONE', #10686, .T. ) ;
#11569=ORIENTED_EDGE ( 'NONE', *, *, #1074, .T. ) ;
#11577=( NAMED_UNIT ( * ) SI_UNIT ( $, .STERADIAN. ) SOLID_ANGLE_UNIT ( ) );
#11580=AXIS2_PLACEMENT_3D ( 'NONE', #7769, #8580, #11583 ) ;
#11583=DIRECTION ( 'NONE',  ( 0.000000000000000000, 0.9998057603070481525, -0.01970892327970900221 ) ) ;
#11608=CARTESIAN_POINT ( 'NONE',  ( 224.4939760857161843, -6.051844909775672576, 0.1192985195352710553 ) ) ;
#11640=FACE_OUTER_BOUND ( 'NONE', #11135, .T. ) ;
#11658=AXIS2_PLACEMENT_3D ( 'NONE', #6000, #9926, #12994 ) ;
#11659=CARTESIAN_POINT ( 'NONE',  ( 227.3999999999999773, 4.447920636657316074, -2.686261716586451520 ) ) ;
#11681=VERTEX_POINT ( 'NONE', #2828 ) ;
#11709=CARTESIAN_POINT ( 'NONE',  ( 235.4000000000000057, 0.000000000000000000, 0.000000000000000000 ) ) ;
#11715=VERTEX_POINT ( 'NONE', #582 ) ;
#11717=CARTESIAN_POINT ( 'NONE',  ( 234.4000000000000057, 0.000000000000000000, 0.000000000000000000 ) ) ;
#11718=AXIS2_PLACEMENT_3D ( 'NONE', #4650, #7595, #474 ) ;
#11720=CARTESIAN_POINT ( 'NONE',  ( 234.4000000000000057, -3.999223041228189057, 0.07883569311883592556 ) ) ;
#11722=DIRECTION ( 'NONE',  ( 0.000000000000000000, 0.9998057603070481525, -0.01970892327970899874 ) ) ;
#11734=FACE_BOUND ( 'NONE', #5553, .T. ) ;
#11739=CARTESIAN_POINT ( 'NONE',  ( 226.7234983661818717, 0.000000000000000000, 0.000000000000000000 ) ) ;
#11748=ORIENTED_EDGE ( 'NONE', *, *, #775, .F. ) ;
#11758=AXIS2_PLACEMENT_3D ( 'NONE', #7309, #9105, #978 ) ;
#11763=VERTEX_POINT ( 'NONE', #3766 ) ;
#11770=CARTESIAN_POINT ( 'NONE',  ( 227.3999999999999773, 2.999417280921144346, -0.05912676983912699968 ) ) ;
#11775=SURFACE_STYLE_USAGE ( .BOTH. , #3827 ) ;
#11790=DIRECTION ( 'NONE',  ( 0.000000000000000000, 0.01970892327970899874, 0.9998057603070481525 ) ) ;
#11792=VECTOR ( 'NONE', #2609, 1000.000000000000114 ) ;
#11798=PRODUCT_DEFINITION_SHAPE ( 'NONE', 'NONE',  #11012 ) ;
#11799=CIRCLE ( 'NONE', #10944, 3.000000000000000000 ) ;
#11803=CIRCLE ( 'NONE', #3700, 2.749999999999999556 ) ;
#11805=CARTESIAN_POINT ( 'NONE',  ( 235.4000000000000057, -3.999223041228192610, 0.07883569311883648068 ) ) ;
#11834=EDGE_LOOP ( 'NONE', ( #10914, #5057, #12556, #3965 ) ) ;
#11851=CARTESIAN_POINT ( 'NONE',  ( 227.3999999999999773, 0.000000000000000000, 0.000000000000000000 ) ) ;
#11857=ORIENTED_EDGE ( 'NONE', *, *, #8934, .T. ) ;
#11885=ORIENTED_EDGE ( 'NONE', *, *, #1353, .F. ) ;
#11910=ADVANCED_FACE ( 'NONE', ( #11640 ), #842, .T. ) ;
#11916=DIRECTION ( 'NONE',  ( 1.000000000000000000, 0.000000000000000000, 0.000000000000000000 ) ) ;
#11919=ADVANCED_FACE ( 'NONE', ( #314 ), #11508, .F. ) ;
#11922=ADVANCED_FACE ( 'NONE', ( #175 ), #8572, .T. ) ;
#11948=CARTESIAN_POINT ( 'NONE',  ( 233.5975020798683204, 0.000000000000000000, 0.000000000000000000 ) ) ;
#11950=CARTESIAN_POINT ( 'NONE',  ( 229.9000000000000057, -4.550331206106116078, -2.508881407069070590 ) ) ;
#11990=ADVANCED_FACE ( 'NONE', ( #3351 ), #7435, .T. ) ;
#12011=ORIENTED_EDGE ( 'NONE', *, *, #2934, .F. ) ;
#12013=DIRECTION ( 'NONE',  ( -1.000000000000000000, 0.000000000000000000, 0.000000000000000000 ) ) ;
#12022=ORIENTED_EDGE ( 'NONE', *, *, #12557, .T. ) ;
#12027=VERTEX_POINT ( 'NONE', #6314 ) ;
#12028=DIRECTION ( 'NONE',  ( 0.000000000000000000, 0.9998057603070481525, -0.01970892327970900221 ) ) ;
#12054=EDGE_LOOP ( 'NONE', ( #1098, #8657, #4485, #3280 ) ) ;
#12070=CARTESIAN_POINT ( 'NONE',  ( 226.7234983661818717, 0.000000000000000000, 0.000000000000000000 ) ) ;
#12071=CARTESIAN_POINT ( 'NONE',  ( 227.3999999999999773, 4.447920636657316074, -2.686261716586451520 ) ) ;
#12085=EDGE_CURVE ( 'NONE', #926, #8770, #3622, .T. ) ;
#12096=VECTOR ( 'NONE', #2411, 1000.000000000000114 ) ;
#12100=ORIENTED_EDGE ( 'NONE', *, *, #2786, .F. ) ;
#12118=VECTOR ( 'NONE', #2457, 1000.000000000000000 ) ;
#12183=EDGE_LOOP ( 'NONE', ( #12982, #7108 ) ) ;
#12215=CONICAL_SURFACE ( 'NONE', #1132, 3.000000000000000000, 0.7853981633974461696 ) ;
#12224=ORIENTED_EDGE ( 'NONE', *, *, #8271, .F. ) ;
#12237=EDGE_LOOP ( 'NONE', ( #5058, #2409, #4042, #10901, #12224 ) ) ;
#12269=CARTESIAN_POINT ( 'NONE',  ( 227.3999999999999773, -0.1281080013181084831, -6.498737441995811714 ) ) ;
#12274=LINE ( 'NONE', #8146, #4167 ) ;
#12276=DIRECTION ( 'NONE',  ( 0.000000000000000000, 0.9998057603070481525, -0.01970892327970899874 ) ) ;
#12287=DIRECTION ( 'NONE',  ( 1.000000000000000000, 0.000000000000000000, 0.000000000000000000 ) ) ;
#12290=AXIS2_PLACEMENT_3D ( 'NONE', #5308, #2651, #4853 ) ;
#12320=TOROIDAL_SURFACE ( 'NONE', #5000, 2.750000000000000000, 0.8000000000000000444 ) ;
#12346=EDGE_CURVE ( 'NONE', #204, #4826, #7448, .T. ) ;
#12358=CARTESIAN_POINT ( 'NONE',  ( 235.4000000000000057, 0.000000000000000000, 0.000000000000000000 ) ) ;
#12380=DIRECTION ( 'NONE',  ( -1.000000000000000000, 0.000000000000000000, 0.000000000000000000 ) ) ;
#12382=CONICAL_SURFACE ( 'NONE', #490, 3.000000000000000000, 0.7853981633974490562 ) ;
#12384=DIRECTION ( 'NONE',  ( 0.000000000000000000, 0.9998057603070480415, -0.01970892327970899527 ) ) ;
#12390=CARTESIAN_POINT ( 'NONE',  ( 235.4000000000000057, -0.1024105694488001289, -5.195143123655522110 ) ) ;
#12396=DIRECTION ( 'NONE',  ( 0.000000000000000000, -0.01970892327970900221, -0.9998057603070482635 ) ) ;
#12401=VERTEX_POINT ( 'NONE', #1070 ) ;
#12425=EDGE_CURVE ( 'NONE', #12854, #4597, #3526, .T. ) ;
#12438=DIRECTION ( 'NONE',  ( 0.000000000000000000, 0.9998057603070480415, -0.01970892327970899874 ) ) ;
#12456=CYLINDRICAL_SURFACE ( 'NONE', #11500, 4.000000000000000000 ) ;
#12469=EDGE_CURVE ( 'NONE', #4826, #204, #3825, .T. ) ;
#12495=DIRECTION ( 'NONE',  ( 0.000000000000000000, 0.9998057603070480415, -0.01970892327970899874 ) ) ;
#12512=DIRECTION ( 'NONE',  ( 0.000000000000000000, 0.9998057603070481525, -0.01970892327970900221 ) ) ;
#12521=SHAPE_REPRESENTATION ( 'Grease Lubrication Injection Nipple', ( #805 ), #5055 ) ;
#12533=CIRCLE ( 'NONE', #7850, 3.000000000000000000 ) ;
#12534=LINE ( 'NONE', #5341, #9438 ) ;
#12538=VECTOR ( 'NONE', #5420, 1000.000000000000114 ) ;
#12541=EDGE_CURVE ( 'NONE', #2702, #4133, #645, .T. ) ;
#12544=ORIENTED_EDGE ( 'NONE', *, *, #8940, .T. ) ;
#12550=LINE ( 'NONE', #298, #9844 ) ;
#12556=ORIENTED_EDGE ( 'NONE', *, *, #4765, .T. ) ;
#12557=EDGE_CURVE ( 'NONE', #3301, #379, #2344, .T. ) ;
#12559=EDGE_CURVE ( 'NONE', #5655, #6838, #10470, .T. ) ;
#12577=ORIENTED_EDGE ( 'NONE', *, *, #938, .T. ) ;
#12594=ORIENTED_EDGE ( 'NONE', *, *, #4626, .F. ) ;
#12617=MECHANICAL_DESIGN_GEOMETRIC_PRESENTATION_REPRESENTATION('',(#3677),#6452);
#12633=ADVANCED_FACE ( 'NONE', ( #1731 ), #10, .F. ) ;
#12640=AXIS2_PLACEMENT_3D ( 'NONE', #2587, #10730, #5334 ) ;
#12645=AXIS2_PLACEMENT_3D ( 'NONE', #13029, #968, #6968 ) ;
#12646=CARTESIAN_POINT ( 'NONE',  ( 235.4000000000000057, 0.000000000000000000, 0.000000000000000000 ) ) ;
#12655=AXIS2_PLACEMENT_3D ( 'NONE', #7462, #12396, #11461 ) ;
#12672=AXIS2_PLACEMENT_3D ( 'NONE', #5584, #6527, #7780 ) ;
#12674=AXIS2_PLACEMENT_3D ( 'NONE', #170, #7168, #9166 ) ;
#12677=ORIENTED_EDGE ( 'NONE', *, *, #3097, .T. ) ;
#12680=ADVANCED_FACE ( 'NONE', ( #8796 ), #863, .F. ) ;
#12683=FACE_OUTER_BOUND ( 'NONE', #8214, .T. ) ;
#12693=CARTESIAN_POINT ( 'NONE',  ( 233.5975020798683204, 2.999417280921144346, -0.05912676983912699968 ) ) ;
#12719=CARTESIAN_POINT ( 'NONE',  ( 229.9000000000000057, 0.1024105694487990187, 5.195143123655512341 ) ) ;
#12724=ADVANCED_FACE ( 'NONE', ( #798 ), #1223, .F. ) ;
#12725=FACE_OUTER_BOUND ( 'NONE', #11517, .T. ) ;
#12733=CARTESIAN_POINT ( 'NONE',  ( 234.4000000000000057, 3.999223041228189057, -0.07883569311883543984 ) ) ;
#12735=AXIS2_PLACEMENT_3D ( 'NONE', #6188, #11242, #12384 ) ;
#12745=AXIS2_PLACEMENT_3D ( 'NONE', #4713, #2525, #6603 ) ;
#12765=CIRCLE ( 'NONE', #8093, 4.500000000000000000 ) ;
#12770=ORIENTED_EDGE ( 'NONE', *, *, #278, .F. ) ;
#12771=VECTOR ( 'NONE', #5404, 1000.000000000000227 ) ;
#12787=DIRECTION ( 'NONE',  ( 1.000000000000000000, 0.000000000000000000, 0.000000000000000000 ) ) ;
#12811=LINE ( 'NONE', #1554, #11792 ) ;
#12815=EDGE_LOOP ( 'NONE', ( #6792, #2874, #8700, #9944, #5489, #11524 ) ) ;
#12838=EDGE_CURVE ( 'NONE', #3738, #3634, #1013, .T. ) ;
#12842=AXIS2_PLACEMENT_3D ( 'NONE', #2557, #3690, #701 ) ;
#12854=VERTEX_POINT ( 'NONE', #5517 ) ;
#12920=EDGE_LOOP ( 'NONE', ( #6422, #9448, #6813, #4612 ) ) ;
#12922=DIRECTION ( 'NONE',  ( 0.000000000000000000, 0.9998057603070481525, -0.01970892327970900221 ) ) ;
#12937=FACE_OUTER_BOUND ( 'NONE', #10442, .T. ) ;
#12940=DIRECTION ( 'NONE',  ( 1.000000000000000000, 0.000000000000000000, 0.000000000000000000 ) ) ;
#12971=ORIENTED_EDGE ( 'NONE', *, *, #9641, .F. ) ;
#12973=ADVANCED_FACE ( 'NONE', ( #4701, #2695 ), #6785, .F. ) ;
#12975=DIRECTION ( 'NONE',  ( 0.000000000000000000, 0.9998057603070480415, -0.01970892327970899874 ) ) ;
#12982=ORIENTED_EDGE ( 'NONE', *, *, #8350, .T. ) ;
#12994=DIRECTION ( 'NONE',  ( 0.000000000000000000, 0.9998057603070481525, -0.01970892327970899874 ) ) ;
#13016=VERTEX_POINT ( 'NONE', #9927 ) ;
#13028=ORIENTED_EDGE ( 'NONE', *, *, #6091, .T. ) ;
#13029=CARTESIAN_POINT ( 'NONE',  ( 233.5975020798683204, -2.199572672675505824, 0.04335963121536006576 ) ) ;
#13038=EDGE_CURVE ( 'NONE', #9134, #5226, #5801, .T. ) ;
ENDSEC;
END-ISO-10303-21;
